ISO-10303-21;
HEADER;
FILE_DESCRIPTION (('STEP AP214'),
    '1' );
FILE_NAME ('14. Nut M6.step',
    '2026-10-09T08:13:37',
    ( '' ),
    ( '' ),
    'SwSTEP 2.0',
    'SolidWorks 2021',
    '' );
FILE_SCHEMA (( 'AUTOMOTIVE_DESIGN' ));
ENDSEC;

DATA;
#15=AXIS2_PLACEMENT_3D ( 'NONE', #14951, #52244, #34992 ) ;
#191=AXIS2_PLACEMENT_3D ( 'NONE', #1829, #61641, #18072 ) ;
#256=CARTESIAN_POINT ( 'NONE',  ( 6.062177826491067734, 2.500000000000000000, 3.500000000000000000 ) ) ;
#274=CARTESIAN_POINT ( 'NONE',  ( 4.041451884327377897, -1.417096231345241097, 7.000000000000000888 ) ) ;
#308=CARTESIAN_POINT ( 'NONE',  ( -4.041451884327380562, 1.417096231345237545, -7.000000000000003553 ) ) ;
#338=EDGE_LOOP ( 'NONE', ( #32374, #30973 ) ) ;
#656=CARTESIAN_POINT ( 'NONE',  ( 0.000000000000000000, -2.500000000000000000, 0.000000000000000000 ) ) ;
#738=ORIENTED_EDGE ( 'NONE', *, *, #6575, .F. ) ;
#745=CARTESIAN_POINT ( 'NONE',  ( 3.673940397442060361E-16, -1.999999999999999556, -3.000000000000000444 ) ) ;
#844=DIRECTION ( 'NONE',  ( 0.000000000000000000, 0.000000000000000000, 1.000000000000000000 ) ) ;
#851=CARTESIAN_POINT ( 'NONE',  ( -7.766391886667105560, 1.733608113333017453, -0.5482146608018624301 ) ) ;
#878=ORIENTED_EDGE ( 'NONE', *, *, #36806, .F. ) ;
#915=CARTESIAN_POINT ( 'NONE',  ( -6.938426666069064552, -2.291132984336068379, 1.982292489777641720 ) ) ;
#966=FACE_OUTER_BOUND ( 'NONE', #59717, .T. ) ;
#1068=CIRCLE ( 'NONE', #41598, 3.499999999999997780 ) ;
#1086=( GEOMETRIC_REPRESENTATION_CONTEXT ( 3 ) GLOBAL_UNCERTAINTY_ASSIGNED_CONTEXT ( ( #3714 ) ) GLOBAL_UNIT_ASSIGNED_CONTEXT ( ( #68652, #21846, #44387 ) ) REPRESENTATION_CONTEXT ( 'NONE', 'WORKASPACE' ) );
#1199=ORIENTED_EDGE ( 'NONE', *, *, #53541, .F. ) ;
#1226=CARTESIAN_POINT ( 'NONE',  ( -5.710692600061824997, -2.499999999999999112, 4.108790270285303414 ) ) ;
#1500=B_SPLINE_CURVE_WITH_KNOTS ( 'NONE', 3,
 ( #35780, #67431, #52658, #4427, #25900, #19931, #18879, #68144 ),
 .UNSPECIFIED., .F., .F.,
 ( 4, 2, 2, 4 ),
 ( 0.004228133357766588295, 0.005276243923116606498, 0.006324354488466623833, 0.008420575619166661974 ),
 .UNSPECIFIED. ) ;
#1576=CARTESIAN_POINT ( 'NONE',  ( -6.062177826491070398, 2.500000000000000000, -3.499999999999998224 ) ) ;
#1614=CARTESIAN_POINT ( 'NONE',  ( -0.7087670488506461197, 2.466410156631503092, -7.000000000000004441 ) ) ;
#1675=ADVANCED_FACE ( 'NONE', ( #48314 ), #22028, .T. ) ;
#1829=CARTESIAN_POINT ( 'NONE',  ( 0.000000000000000000, -2.500000000000000000, 0.000000000000000000 ) ) ;
#2083=AXIS2_PLACEMENT_3D ( 'NONE', #26863, #31824, #52958 ) ;
#2298=AXIS2_PLACEMENT_3D ( 'NONE', #52152, #36331, #31336 ) ;
#2425=CIRCLE ( 'NONE', #41751, 6.999999999999997335 ) ;
#2530=CARTESIAN_POINT ( 'NONE',  ( 6.938426666069061000, 2.291132984336068823, -1.982292489777642164 ) ) ;
#2651=B_SPLINE_CURVE_WITH_KNOTS ( 'NONE', 3,
 ( #33285, #22037, #64604, #32943, #43540, #49469, #16778, #65633 ),
 .UNSPECIFIED., .F., .F.,
 ( 4, 2, 2, 4 ),
 ( 2.544316211733585141E-07, 0.002094919859796805575, 0.003142252573884622441, 0.004189585287972440175 ),
 .UNSPECIFIED. ) ;
#2710=EDGE_LOOP ( 'NONE', ( #13803, #11245, #54789, #8873, #61232, #35732 ) ) ;
#2895=DIRECTION ( 'NONE',  ( 0.000000000000000000, 1.000000000000000000, 0.000000000000000000 ) ) ;
#3057=CARTESIAN_POINT ( 'NONE',  ( 7.440601873764704166, -2.005109422339667269, 1.112499515747340073 ) ) ;
#3096=CARTESIAN_POINT ( 'NONE',  ( 3.728455551739338514, 1.573594397639262343, 7.000000000000000888 ) ) ;
#3132=PLANE ( 'NONE',  #13797 ) ;
#3545=CARTESIAN_POINT ( 'NONE',  ( 0.000000000000000000, -2.500000000000000000, 0.000000000000000000 ) ) ;
#3593=AXIS2_PLACEMENT_3D ( 'NONE', #52061, #14064, #56968 ) ;
#3601=DIRECTION ( 'NONE',  ( -0.000000000000000000, -1.000000000000000000, -0.000000000000000000 ) ) ;
#3602=CARTESIAN_POINT ( 'NONE',  ( -6.062177826491069510, 2.500000000000000000, 3.499999999999999556 ) ) ;
#3714=UNCERTAINTY_MEASURE_WITH_UNIT (LENGTH_MEASURE( 1.000000000000000082E-05 ), #68652, 'distance_accuracy_value', 'NONE');
#3728=AXIS2_PLACEMENT_3D ( 'NONE', #34311, #7570, #17794 ) ;
#3748=VERTEX_POINT ( 'NONE', #28522 ) ;
#3861=EDGE_LOOP ( 'NONE', ( #1199, #33181, #50194, #9344, #40824, #24708 ) ) ;
#3898=CONICAL_SURFACE ( 'NONE', #57867, 6.999999999999997335, 0.7853981633974500554 ) ;
#3943=( NAMED_UNIT ( * ) PLANE_ANGLE_UNIT ( ) SI_UNIT ( $, .RADIAN. ) );
#4161=ORIENTED_EDGE ( 'NONE', *, *, #23903, .F. ) ;
#4242=VERTEX_POINT ( 'NONE', #37242 ) ;
#4427=CARTESIAN_POINT ( 'NONE',  ( 2.755156416453792279, -1.983268963954967434, -7.000000000000002665 ) ) ;
#4507=CARTESIAN_POINT ( 'NONE',  ( -1.233556390963996163, -2.406758536253310155, -7.000000000000001776 ) ) ;
#4656=ADVANCED_FACE ( 'NONE', ( #53969, #49092 ), #31472, .T. ) ;
#4679=CARTESIAN_POINT ( 'NONE',  ( -8.082903768654761123, 2.500000000000000000, -1.781658826789683271E-15 ) ) ;
#4778=EDGE_CURVE ( 'NONE', #3748, #39091, #61674, .T. ) ;
#4906=ORIENTED_EDGE ( 'NONE', *, *, #55980, .T. ) ;
#4994=SURFACE_STYLE_USAGE ( .BOTH. , #36719 ) ;
#4998=EDGE_CURVE ( 'NONE', #58318, #15154, #54321, .T. ) ;
#5287=FACE_OUTER_BOUND ( 'NONE', #51265, .T. ) ;
#5291=CARTESIAN_POINT ( 'NONE',  ( -8.082903768654761123, 1.417096231345241097, -1.759977097422839922E-15 ) ) ;
#5653=DIRECTION ( 'NONE',  ( 0.000000000000000000, 1.000000000000000000, 0.000000000000000000 ) ) ;
#5859=DIRECTION ( 'NONE',  ( -0.000000000000000000, -1.000000000000000000, -0.000000000000000000 ) ) ;
#6001=ORIENTED_EDGE ( 'NONE', *, *, #33839, .F. ) ;
#6048=FACE_OUTER_BOUND ( 'NONE', #14622, .T. ) ;
#6140=ORIENTED_EDGE ( 'NONE', *, *, #52011, .F. ) ;
#6202=B_SPLINE_CURVE_WITH_KNOTS ( 'NONE', 3,
 ( #51728, #22131, #37670, #27379, #16879, #69293, #21087, #256 ),
 .UNSPECIFIED., .F., .F.,
 ( 4, 2, 2, 4 ),
 ( 2.544316211733585141E-07, 0.002094919859796804708, 0.003142252573884620707, 0.004189585287972436706 ),
 .UNSPECIFIED. ) ;
#6283=VERTEX_POINT ( 'NONE', #16287 ) ;
#6462=EDGE_LOOP ( 'NONE', ( #9776, #10021, #25729 ) ) ;
#6494=CARTESIAN_POINT ( 'NONE',  ( -4.041451884327380562, 2.500000000000000000, -7.000000000000003553 ) ) ;
#6549=AXIS2_PLACEMENT_3D ( 'NONE', #40973, #8928, #40613 ) ;
#6575=EDGE_CURVE ( 'NONE', #10734, #34321, #6202, .T. ) ;
#6878=DIRECTION ( 'NONE',  ( 0.000000000000000000, 0.000000000000000000, 1.000000000000000000 ) ) ;
#6911=CARTESIAN_POINT ( 'NONE',  ( -4.357963766315032572, -1.733608113333017453, 6.451785339198141678 ) ) ;
#7079=LINE ( 'NONE', #38785, #55849 ) ;
#7217=DIRECTION ( 'NONE',  ( 0.000000000000000000, 0.000000000000000000, 1.000000000000000000 ) ) ;
#7270=CARTESIAN_POINT ( 'NONE',  ( 2.755156416437880562, -1.983268963961026810, 7.000000000000000000 ) ) ;
#7277=CARTESIAN_POINT ( 'NONE',  ( -4.041451884327378785, 1.417096231345241542, 7.000000000000000000 ) ) ;
#7302=CARTESIAN_POINT ( 'NONE',  ( -4.041451884327380562, 1.417096231345237545, -7.000000000000003553 ) ) ;
#7374=B_SPLINE_CURVE_WITH_KNOTS ( 'NONE', 3,
 ( #17533, #23813, #51253, #1614, #23140, #18864, #44630, #66027, #7302 ),
 .UNSPECIFIED., .F., .F.,
 ( 4, 2, 1, 2, 4 ),
 ( 0.008420575619166656769, 0.008943833652465342163, 0.009467091685764029291, 0.01051360775236140181, 0.01260663988555614685 ),
 .UNSPECIFIED. ) ;
#7376=ORIENTED_EDGE ( 'NONE', *, *, #39756, .T. ) ;
#7461=CARTESIAN_POINT ( 'NONE',  ( 0.000000000000000000, -2.500000000000000000, 0.000000000000000000 ) ) ;
#7570=DIRECTION ( 'NONE',  ( -1.073081856240828813E-16, 0.000000000000000000, 1.000000000000000000 ) ) ;
#7812=DIRECTION ( 'NONE',  ( 0.000000000000000000, 0.000000000000000000, 1.000000000000000000 ) ) ;
#7890=MECHANICAL_DESIGN_GEOMETRIC_PRESENTATION_REPRESENTATION('',(#30308),#34856);
#7911=VERTEX_POINT ( 'NONE', #62187 ) ;
#8040=EDGE_LOOP ( 'NONE', ( #9526, #13445, #65812 ) ) ;
#8131=DIRECTION ( 'NONE',  ( 0.000000000000000000, 0.000000000000000000, 1.000000000000000000 ) ) ;
#8181=CARTESIAN_POINT ( 'NONE',  ( 0.000000000000000000, -2.500000000000000000, 0.000000000000000000 ) ) ;
#8192=ADVANCED_FACE ( 'NONE', ( #34435 ), #3898, .T. ) ;
#8222=CARTESIAN_POINT ( 'NONE',  ( 8.082903768654761123, 1.417096231345241097, 9.294316082458970795E-16 ) ) ;
#8265=CIRCLE ( 'NONE', #18403, 6.999999999999997335 ) ;
#8317=CARTESIAN_POINT ( 'NONE',  ( 2.418047948263830627, -2.101261491288919814, 7.000000000000000000 ) ) ;
#8325=CARTESIAN_POINT ( 'NONE',  ( -3.414270897520785386, 1.730686724748536021, 7.000000000000000000 ) ) ;
#8459=CARTESIAN_POINT ( 'NONE',  ( 4.041451884327377897, 1.417096231345241319, 7.000000000000000888 ) ) ;
#8535=ORIENTED_EDGE ( 'NONE', *, *, #64872, .F. ) ;
#8610=MECHANICAL_DESIGN_GEOMETRIC_PRESENTATION_REPRESENTATION('',(#44597),#13068);
#8873=ORIENTED_EDGE ( 'NONE', *, *, #49992, .F. ) ;
#8893=FILL_AREA_STYLE ('',( #15252 ) ) ;
#8928=DIRECTION ( 'NONE',  ( 0.000000000000000000, 1.000000000000000000, 0.000000000000000000 ) ) ;
#8929=CARTESIAN_POINT ( 'NONE',  ( -6.767634268437465295, 2.367558512213881361, 2.278113600022078078 ) ) ;
#8930=CIRCLE ( 'NONE', #16834, 6.999999999999997335 ) ;
#9053=ADVANCED_FACE ( 'NONE', ( #54364 ), #49133, .F. ) ;
#9240=CARTESIAN_POINT ( 'NONE',  ( 8.082903768654761123, 2.500000000000000000, 9.511133375893962597E-16 ) ) ;
#9344=ORIENTED_EDGE ( 'NONE', *, *, #60204, .T. ) ;
#9515=CARTESIAN_POINT ( 'NONE',  ( 6.062177826491067734, 2.500000000000000000, 3.500000000000000000 ) ) ;
#9526=ORIENTED_EDGE ( 'NONE', *, *, #65403, .T. ) ;
#9647=CARTESIAN_POINT ( 'NONE',  ( -8.082903768654761123, 1.417096231345241097, -1.759977097422839922E-15 ) ) ;
#9776=ORIENTED_EDGE ( 'NONE', *, *, #32031, .T. ) ;
#9797=CARTESIAN_POINT ( 'NONE',  ( 3.673940397442060361E-16, 2.000000000000000444, -3.000000000000000444 ) ) ;
#10021=ORIENTED_EDGE ( 'NONE', *, *, #13254, .T. ) ;
#10049=CONICAL_SURFACE ( 'NONE', #30241, 6.999999999999997335, 0.7853981633974500554 ) ;
#10142=FACE_OUTER_BOUND ( 'NONE', #56761, .T. ) ;
#10164=CARTESIAN_POINT ( 'NONE',  ( -0.7087670488506471189, -2.466410156631502648, -7.000000000000002665 ) ) ;
#10172=FACE_OUTER_BOUND ( 'NONE', #37114, .T. ) ;
#10187=CARTESIAN_POINT ( 'NONE',  ( 7.440601873764704166, 2.005109422339667269, 1.112499515747340073 ) ) ;
#10396=CARTESIAN_POINT ( 'NONE',  ( 4.286263797015740046E-16, 2.500000000000000000, -3.500000000000003553 ) ) ;
#10433=CARTESIAN_POINT ( 'NONE',  ( 4.041451884327377897, 2.500000000000000000, 7.000000000000000888 ) ) ;
#10459=ADVANCED_FACE ( 'NONE', ( #17491 ), #10049, .T. ) ;
#10492=EDGE_CURVE ( 'NONE', #37645, #15154, #12510, .T. ) ;
#10514=CARTESIAN_POINT ( 'NONE',  ( 7.511572993685799101E-16, -2.500000000000000000, -6.999999999999997335 ) ) ;
#10518=CARTESIAN_POINT ( 'NONE',  ( 8.082903768654761123, -1.417096231345241097, 9.294316082458970795E-16 ) ) ;
#10572=CARTESIAN_POINT ( 'NONE',  ( -5.365183871890740974, 2.392512705203733159, 4.707228941936125288 ) ) ;
#10579=EDGE_CURVE ( 'NONE', #67895, #63907, #24623, .T. ) ;
#10611=B_SPLINE_CURVE_WITH_KNOTS ( 'NONE', 3,
 ( #10514, #47499, #59350, #10164, #4507, #31598, #48521, #32292, #53081 ),
 .UNSPECIFIED., .F., .F.,
 ( 4, 2, 1, 2, 4 ),
 ( 0.008420575619166661974, 0.008943833652465347367, 0.009467091685764034495, 0.01051360775236140702, 0.01260663988555615379 ),
 .UNSPECIFIED. ) ;
#10734=VERTEX_POINT ( 'NONE', #36463 ) ;
#10830=DIRECTION ( 'NONE',  ( 0.000000000000000000, 0.000000000000000000, 1.000000000000000000 ) ) ;
#11245=ORIENTED_EDGE ( 'NONE', *, *, #52862, .T. ) ;
#11285=DIRECTION ( 'NONE',  ( 0.000000000000000000, 1.000000000000000000, 0.000000000000000000 ) ) ;
#11760=CARTESIAN_POINT ( 'NONE',  ( 0.7093150608672392776, 2.499999999999994227, -7.000000000000001776 ) ) ;
#11884=EDGE_LOOP ( 'NONE', ( #15567, #38959, #53398, #31440 ) ) ;
#11964=COLOUR_RGB ( '', 0.08235294, 0.09019608, 0.10196078) ;
#11965=CARTESIAN_POINT ( 'NONE',  ( -5.885195493260865440, 2.499999999999996447, -3.806542393196803431 ) ) ;
#11977=ORIENTED_EDGE ( 'NONE', *, *, #65674, .F. ) ;
#11984=ORIENTED_EDGE ( 'NONE', *, *, #13495, .F. ) ;
#12140=EDGE_LOOP ( 'NONE', ( #38769, #44147, #8535 ) ) ;
#12199=EDGE_CURVE ( 'NONE', #30149, #28517, #25695, .T. ) ;
#12203=ORIENTED_EDGE ( 'NONE', *, *, #37448, .T. ) ;
#12400=ORIENTED_EDGE ( 'NONE', *, *, #4998, .T. ) ;
#12510=LINE ( 'NONE', #54391, #66200 ) ;
#12583=CARTESIAN_POINT ( 'NONE',  ( -6.062177826491069510, -2.500000000000000000, 3.499999999999999556 ) ) ;
#12648=CARTESIAN_POINT ( 'NONE',  ( -5.705565085145811288, 2.472216779103303175, -4.117671386636410524 ) ) ;
#12666=CARTESIAN_POINT ( 'NONE',  ( 7.511572993685799101E-16, -2.500000000000000000, -6.999999999999997335 ) ) ;
#12722=DIRECTION ( 'NONE',  ( -0.000000000000000000, -1.000000000000000000, -0.000000000000000000 ) ) ;
#12794=VERTEX_POINT ( 'NONE', #31497 ) ;
#12827=FACE_OUTER_BOUND ( 'NONE', #50680, .T. ) ;
#12878=CARTESIAN_POINT ( 'NONE',  ( 1.400957079539665084, -2.390838073342431702, 7.000000000000000888 ) ) ;
#12926=AXIS2_PLACEMENT_3D ( 'NONE', #6494, #27937, #55035 ) ;
#12961=DIRECTION ( 'NONE',  ( -0.000000000000000000, -1.000000000000000000, -0.000000000000000000 ) ) ;
#12971=ORIENTED_EDGE ( 'NONE', *, *, #34383, .T. ) ;
#12983=EDGE_CURVE ( 'NONE', #12794, #28517, #32764, .T. ) ;
#12999=CARTESIAN_POINT ( 'NONE',  ( -6.062177826491070398, 2.500000000000000000, -3.499999999999998224 ) ) ;
#13068=( GEOMETRIC_REPRESENTATION_CONTEXT ( 3 ) GLOBAL_UNCERTAINTY_ASSIGNED_CONTEXT ( ( #51083 ) ) GLOBAL_UNIT_ASSIGNED_CONTEXT ( ( #19792, #3943, #37056 ) ) REPRESENTATION_CONTEXT ( 'NONE', 'WORKASPACE' ) );
#13248=FACE_OUTER_BOUND ( 'NONE', #11884, .T. ) ;
#13254=EDGE_CURVE ( 'NONE', #30142, #25818, #30914, .T. ) ;
#13300=ORIENTED_EDGE ( 'NONE', *, *, #59279, .T. ) ;
#13445=ORIENTED_EDGE ( 'NONE', *, *, #47865, .T. ) ;
#13495=EDGE_CURVE ( 'NONE', #51146, #7911, #2425, .T. ) ;
#13533=EDGE_LOOP ( 'NONE', ( #27707, #43286, #29377, #27288 ) ) ;
#13662=B_SPLINE_CURVE_WITH_KNOTS ( 'NONE', 3,
 ( #17071, #38550, #48756, #54318, #49756, #47460, #11760, #23023 ),
 .UNSPECIFIED., .F., .F.,
 ( 4, 2, 2, 4 ),
 ( 0.004228133357766583958, 0.005276243923116602161, 0.006324354488466620364, 0.008420575619166656769 ),
 .UNSPECIFIED. ) ;
#13760=VERTEX_POINT ( 'NONE', #44291 ) ;
#13797=AXIS2_PLACEMENT_3D ( 'NONE', #41214, #45111, #45467 ) ;
#13803=ORIENTED_EDGE ( 'NONE', *, *, #10492, .T. ) ;
#13893=ADVANCED_FACE ( 'NONE', ( #13248 ), #26700, .F. ) ;
#13984=AXIS2_PLACEMENT_3D ( 'NONE', #49284, #11285, #32740 ) ;
#14064=DIRECTION ( 'NONE',  ( 0.000000000000000000, -1.000000000000000000, 0.000000000000000000 ) ) ;
#14076=ORIENTED_EDGE ( 'NONE', *, *, #39579, .F. ) ;
#14191=CARTESIAN_POINT ( 'NONE',  ( 6.767634268437461742, 2.367558512213881805, -2.278113600022080298 ) ) ;
#14253=CARTESIAN_POINT ( 'NONE',  ( -4.041451884327380562, -1.417096231345237545, -7.000000000000003553 ) ) ;
#14274=CARTESIAN_POINT ( 'NONE',  ( 4.041451884327377897, -1.417096231345241097, 7.000000000000000888 ) ) ;
#14331=ORIENTED_EDGE ( 'NONE', *, *, #13254, .F. ) ;
#14622=EDGE_LOOP ( 'NONE', ( #31263, #17245, #59358, #23948 ) ) ;
#14836=DIRECTION ( 'NONE',  ( 0.000000000000000000, -1.000000000000000000, 0.000000000000000000 ) ) ;
#14854=ORIENTED_EDGE ( 'NONE', *, *, #65403, .F. ) ;
#14861=DIRECTION ( 'NONE',  ( 0.000000000000000000, 0.000000000000000000, 1.000000000000000000 ) ) ;
#14888=EDGE_CURVE ( 'NONE', #51313, #67895, #61052, .T. ) ;
#14911=DIRECTION ( 'NONE',  ( 0.000000000000000000, 0.000000000000000000, 1.000000000000000000 ) ) ;
#14917=ORIENTED_EDGE ( 'NONE', *, *, #61758, .F. ) ;
#14951=CARTESIAN_POINT ( 'NONE',  ( 0.000000000000000000, -2.500000000000000000, 0.000000000000000000 ) ) ;
#14982=CIRCLE ( 'NONE', #56513, 6.999999999999997335 ) ;
#15039=DIRECTION ( 'NONE',  ( -0.000000000000000000, -1.000000000000000000, -0.000000000000000000 ) ) ;
#15154=VERTEX_POINT ( 'NONE', #23292 ) ;
#15221=ADVANCED_FACE ( 'NONE', ( #51075 ), #43835, .T. ) ;
#15252=FILL_AREA_STYLE_COLOUR ( '', #11964 ) ;
#15439=EDGE_LOOP ( 'NONE', ( #37217, #52852, #46844, #35159 ) ) ;
#15501=CIRCLE ( 'NONE', #38053, 3.000000000000000444 ) ;
#15518=ORIENTED_EDGE ( 'NONE', *, *, #66650, .T. ) ;
#15567=ORIENTED_EDGE ( 'NONE', *, *, #40619, .F. ) ;
#15939=CARTESIAN_POINT ( 'NONE',  ( 4.041451884327375232, 1.417096231345241097, -7.000000000000002665 ) ) ;
#16024=CONICAL_SURFACE ( 'NONE', #3593, 6.999999999999997335, 0.7853981633974500554 ) ;
#16038=DIRECTION ( 'NONE',  ( 0.000000000000000000, 0.000000000000000000, 1.000000000000000000 ) ) ;
#16125=CARTESIAN_POINT ( 'NONE',  ( 0.000000000000000000, 2.500000000000000000, 0.000000000000000000 ) ) ;
#16257=ADVANCED_FACE ( 'NONE', ( #5287 ), #19067, .F. ) ;
#16269=DIRECTION ( 'NONE',  ( 0.000000000000000000, 1.000000000000000000, 0.000000000000000000 ) ) ;
#16287=CARTESIAN_POINT ( 'NONE',  ( -7.511572993685798115E-16, -2.500000000000000000, 6.999999999999997335 ) ) ;
#16372=ORIENTED_EDGE ( 'NONE', *, *, #38213, .F. ) ;
#16574=AXIS2_PLACEMENT_3D ( 'NONE', #49482, #60356, #844 ) ;
#16575=EDGE_CURVE ( 'NONE', #30495, #45750, #10611, .T. ) ;
#16589=CARTESIAN_POINT ( 'NONE',  ( -4.682380833558966060, 2.003239292658526516, -5.889878495889164789 ) ) ;
#16685=CARTESIAN_POINT ( 'NONE',  ( 0.000000000000000000, -2.500000000000000000, 0.000000000000000000 ) ) ;
#16740=CARTESIAN_POINT ( 'NONE',  ( 4.286263797015733637E-16, -2.500000000000000000, 3.499999999999997780 ) ) ;
#16778=CARTESIAN_POINT ( 'NONE',  ( -5.885195493260865440, -2.499999999999996447, -3.806542393196803431 ) ) ;
#16811=APPLICATION_CONTEXT ( 'automotive_design' ) ;
#16834=AXIS2_PLACEMENT_3D ( 'NONE', #7461, #12722, #38817 ) ;
#16841=AXIS2_PLACEMENT_3D ( 'NONE', #16685, #23652, #44132 ) ;
#16879=CARTESIAN_POINT ( 'NONE',  ( 5.356721384544673725, 2.367558512213880473, 4.721886399977921478 ) ) ;
#16978=DIRECTION ( 'NONE',  ( 0.000000000000000000, 0.000000000000000000, 1.000000000000000000 ) ) ;
#17071=CARTESIAN_POINT ( 'NONE',  ( 4.041451884327375232, 1.417096231345241097, -7.000000000000002665 ) ) ;
#17152=CARTESIAN_POINT ( 'NONE',  ( -7.440601873764705054, 2.005109422339667269, -1.112499515747341183 ) ) ;
#17198=FACE_OUTER_BOUND ( 'NONE', #45333, .T. ) ;
#17245=ORIENTED_EDGE ( 'NONE', *, *, #36499, .F. ) ;
#17491=FACE_OUTER_BOUND ( 'NONE', #8040, .T. ) ;
#17533=CARTESIAN_POINT ( 'NONE',  ( 7.511572993685799101E-16, 2.500000000000000000, -6.999999999999997335 ) ) ;
#17607=DIRECTION ( 'NONE',  ( 0.000000000000000000, 0.000000000000000000, 1.000000000000000000 ) ) ;
#17679=ORIENTED_EDGE ( 'NONE', *, *, #14888, .T. ) ;
#17746=ORIENTED_EDGE ( 'NONE', *, *, #19280, .F. ) ;
#17794=DIRECTION ( 'NONE',  ( 1.000000000000000000, 0.000000000000000000, 1.073081856240828813E-16 ) ) ;
#17816=DIRECTION ( 'NONE',  ( 0.000000000000000000, 1.000000000000000000, 0.000000000000000000 ) ) ;
#17881=DIRECTION ( 'NONE',  ( 0.000000000000000000, 1.000000000000000000, 0.000000000000000000 ) ) ;
#17914=CARTESIAN_POINT ( 'NONE',  ( 4.041451884327375232, -1.417096231345241097, -7.000000000000002665 ) ) ;
#17938=CARTESIAN_POINT ( 'NONE',  ( -5.356721384544675502, 2.367558512213879141, -4.721886399977922366 ) ) ;
#17944=( LENGTH_UNIT ( ) NAMED_UNIT ( * ) SI_UNIT ( .MILLI., .METRE. ) );
#18072=DIRECTION ( 'NONE',  ( 0.000000000000000000, -0.000000000000000000, 1.000000000000000000 ) ) ;
#18255=CARTESIAN_POINT ( 'NONE',  ( -1.745454270669493990, -2.292880170259729233, 7.000000000000000000 ) ) ;
#18272=ADVANCED_FACE ( 'NONE', ( #47994 ), #58152, .F. ) ;
#18403=AXIS2_PLACEMENT_3D ( 'NONE', #44311, #48542, #31968 ) ;
#18426=AXIS2_PLACEMENT_3D ( 'NONE', #41732, #42439, #16038 ) ;
#18465=DIRECTION ( 'NONE',  ( 0.000000000000000000, 1.000000000000000000, 0.000000000000000000 ) ) ;
#18524=CARTESIAN_POINT ( 'NONE',  ( -1.745454270669494212, 2.292880170259729233, 7.000000000000000000 ) ) ;
#18760=CARTESIAN_POINT ( 'NONE',  ( 6.418790567836325955, 2.472216779103306283, -2.882328613363592584 ) ) ;
#18864=CARTESIAN_POINT ( 'NONE',  ( -1.745454270680676157, 2.292880170256995420, -7.000000000000005329 ) ) ;
#18879=CARTESIAN_POINT ( 'NONE',  ( 0.7093150608672396107, -2.499999999999996003, -7.000000000000007105 ) ) ;
#18911=CARTESIAN_POINT ( 'NONE',  ( 0.000000000000000000, -1.999999999999999556, 0.000000000000000000 ) ) ;
#18917=B_SPLINE_CURVE_WITH_KNOTS ( 'NONE', 3,
 ( #41516, #56973, #45761, #29543, #57315, #51012, #3096, #8459 ),
 .UNSPECIFIED., .F., .F.,
 ( 4, 2, 2, 4 ),
 ( 0.01183260977662614448, 0.01392219916432753390, 0.01496699385817822948, 0.01601178855202892506 ),
 .UNSPECIFIED. ) ;
#18933=B_SPLINE_CURVE_WITH_KNOTS ( 'NONE', 3,
 ( #40783, #29501, #57271, #3057, #66807, #61488 ),
 .UNSPECIFIED., .F., .F.,
 ( 4, 2, 4 ),
 ( 0.004189585287972436706, 0.006269578072783809838, 0.008349570857595182971 ),
 .UNSPECIFIED. ) ;
#19064=AXIS2_PLACEMENT_3D ( 'NONE', #57384, #14836, #45816 ) ;
#19067=CONICAL_SURFACE ( 'NONE', #49438, 3.499999999999997780, 0.7853981633974452814 ) ;
#19226=B_SPLINE_CURVE_WITH_KNOTS ( 'NONE', 3,
 ( #10518, #22098, #26652, #33002, #32295, #64671, #38316, #36929 ),
 .UNSPECIFIED., .F., .F.,
 ( 4, 2, 2, 4 ),
 ( 2.544316211735810720E-07, 0.002094919859796807744, 0.003142252573884624176, 0.004189585287972440175 ),
 .UNSPECIFIED. ) ;
#19280=EDGE_CURVE ( 'NONE', #13760, #12794, #61073, .T. ) ;
#19541=CARTESIAN_POINT ( 'NONE',  ( 0.7093150608870643081, -2.499999999999996891, 7.000000000000000888 ) ) ;
#19578=DIRECTION ( 'NONE',  ( 0.000000000000000000, 0.000000000000000000, 1.000000000000000000 ) ) ;
#19666=DIRECTION ( 'NONE',  ( 0.000000000000000000, 0.000000000000000000, 1.000000000000000000 ) ) ;
#19792=( LENGTH_UNIT ( ) NAMED_UNIT ( * ) SI_UNIT ( .MILLI., .METRE. ) );
#19931=CARTESIAN_POINT ( 'NONE',  ( 1.400957079523477589, -2.390838073347307802, -7.000000000000005329 ) ) ;
#20041=CARTESIAN_POINT ( 'NONE',  ( 0.000000000000000000, 2.500000000000000000, 0.000000000000000000 ) ) ;
#20136=ORIENTED_EDGE ( 'NONE', *, *, #37448, .F. ) ;
#20156=CARTESIAN_POINT ( 'NONE',  ( -7.441974819423173848, 2.003239292658529180, 1.110121504110835877 ) ) ;
#20210=CARTESIAN_POINT ( 'NONE',  ( 8.082903768654761123, 1.417096231345241097, 9.294316082458970795E-16 ) ) ;
#20225=VECTOR ( 'NONE', #15039, 1000.000000000000000 ) ;
#20496=CARTESIAN_POINT ( 'NONE',  ( -8.082903768654761123, -1.417096231345241097, -1.759977097422839922E-15 ) ) ;
#20894=ORIENTED_EDGE ( 'NONE', *, *, #34383, .F. ) ;
#20912=ORIENTED_EDGE ( 'NONE', *, *, #4778, .F. ) ;
#21033=DIRECTION ( 'NONE',  ( 0.000000000000000000, 1.000000000000000000, 0.000000000000000000 ) ) ;
#21087=CARTESIAN_POINT ( 'NONE',  ( 5.885195493260862776, 2.499999999999998668, 3.806542393196804763 ) ) ;
#21124=CARTESIAN_POINT ( 'NONE',  ( 3.673940397442060361E-16, -2.500000000000000000, -3.000000000000000444 ) ) ;
#21206=ADVANCED_FACE ( 'NONE', ( #61696 ), #52583, .F. ) ;
#21465=CONICAL_SURFACE ( 'NONE', #28153, 6.999999999999997335, 0.7853981633974500554 ) ;
#21494=CARTESIAN_POINT ( 'NONE',  ( 4.041451884327377897, -1.417096231345241097, 7.000000000000000888 ) ) ;
#21759=ORIENTED_EDGE ( 'NONE', *, *, #38213, .T. ) ;
#21794=PLANE ( 'NONE',  #57019 ) ;
#21823=AXIS2_PLACEMENT_3D ( 'NONE', #33610, #38938, #6878 ) ;
#21846=( NAMED_UNIT ( * ) PLANE_ANGLE_UNIT ( ) SI_UNIT ( $, .RADIAN. ) );
#22028=CONICAL_SURFACE ( 'NONE', #35493, 6.999999999999997335, 0.7853981633974500554 ) ;
#22037=CARTESIAN_POINT ( 'NONE',  ( -4.358330484967981810, -1.733974831985838794, -6.451150163859153963 ) ) ;
#22045=ORIENTED_EDGE ( 'NONE', *, *, #65025, .T. ) ;
#22098=CARTESIAN_POINT ( 'NONE',  ( 7.766025168014159874, -1.733974831985843013, -0.5488498361408489234 ) ) ;
#22131=CARTESIAN_POINT ( 'NONE',  ( 4.358330484967978258, 1.733974831985841458, 6.451150163859151299 ) ) ;
#22199=CARTESIAN_POINT ( 'NONE',  ( 0.000000000000000000, 2.500000000000000000, 0.000000000000000000 ) ) ;
#22363=CONICAL_SURFACE ( 'NONE', #61649, 6.999999999999997335, 0.7853981633974500554 ) ;
#22495=ORIENTED_EDGE ( 'NONE', *, *, #62179, .T. ) ;
#22756=CARTESIAN_POINT ( 'NONE',  ( -4.683753779217433078, -2.005109422339666825, 5.887500484252660371 ) ) ;
#22890=SHAPE_REPRESENTATION_RELATIONSHIP ( 'NONE' , 'NONE' ,  #60355, #25286 ) ;
#22899=AXIS2_PLACEMENT_3D ( 'NONE', #18911, #12961, #29484 ) ;
#22993=CIRCLE ( 'NONE', #62303, 6.999999999999997335 ) ;
#23023=CARTESIAN_POINT ( 'NONE',  ( 7.511572993685799101E-16, 2.500000000000000000, -6.999999999999997335 ) ) ;
#23102=CARTESIAN_POINT ( 'NONE',  ( -8.082903768654761123, 1.417096231345241097, -1.759977097422839922E-15 ) ) ;
#23140=CARTESIAN_POINT ( 'NONE',  ( -1.233556390963994831, 2.406758536253309710, -7.000000000000002665 ) ) ;
#23172=ORIENTED_EDGE ( 'NONE', *, *, #46096, .F. ) ;
#23289=ORIENTED_EDGE ( 'NONE', *, *, #55750, .F. ) ;
#23292=CARTESIAN_POINT ( 'NONE',  ( 4.041451884327375232, -1.417096231345241097, -7.000000000000002665 ) ) ;
#23315=CARTESIAN_POINT ( 'NONE',  ( -4.041451884327380562, 1.417096231345237545, -7.000000000000003553 ) ) ;
#23386=PRODUCT_CONTEXT ( 'NONE', #37069, 'mechanical' ) ;
#23462=DIRECTION ( 'NONE',  ( 0.000000000000000000, 1.000000000000000000, 0.000000000000000000 ) ) ;
#23608=CARTESIAN_POINT ( 'NONE',  ( 0.000000000000000000, -2.500000000000000000, -3.499999999999997780 ) ) ;
#23635=CARTESIAN_POINT ( 'NONE',  ( -6.062177826491069510, 2.500000000000000000, 3.499999999999999556 ) ) ;
#23652=DIRECTION ( 'NONE',  ( -0.000000000000000000, -1.000000000000000000, -0.000000000000000000 ) ) ;
#23689=DIRECTION ( 'NONE',  ( -0.000000000000000000, -1.000000000000000000, -0.000000000000000000 ) ) ;
#23813=CARTESIAN_POINT ( 'NONE',  ( -0.1770589935874656851, 2.499999999999994227, -7.000000000000004441 ) ) ;
#23875=CARTESIAN_POINT ( 'NONE',  ( 4.357963766315029019, -1.733608113333017897, -6.451785339198144342 ) ) ;
#23903=EDGE_CURVE ( 'NONE', #7911, #4242, #28099, .T. ) ;
#23948=ORIENTED_EDGE ( 'NONE', *, *, #39165, .F. ) ;
#24289=CARTESIAN_POINT ( 'NONE',  ( -4.041451884327378785, 2.500000000000000000, 7.000000000000000000 ) ) ;
#24296=LINE ( 'NONE', #23608, #54255 ) ;
#24337=ORIENTED_EDGE ( 'NONE', *, *, #36806, .T. ) ;
#24373=CARTESIAN_POINT ( 'NONE',  ( 6.062177826491068622, 2.500000000000000000, -3.500000000000001332 ) ) ;
#24428=VERTEX_POINT ( 'NONE', #33884 ) ;
#24445=ADVANCED_FACE ( 'NONE', ( #67299, #56033 ), #50100, .F. ) ;
#24462=CARTESIAN_POINT ( 'NONE',  ( -0.1770589935948753968, 2.499999999999996891, 7.000000000000000000 ) ) ;
#24623=CIRCLE ( 'NONE', #35902, 6.999999999999997335 ) ;
#24708=ORIENTED_EDGE ( 'NONE', *, *, #61758, .T. ) ;
#24721=FACE_OUTER_BOUND ( 'NONE', #12140, .T. ) ;
#24770=ADVANCED_FACE ( 'NONE', ( #6048 ), #28295, .F. ) ;
#25049=DIRECTION ( 'NONE',  ( 0.000000000000000000, 1.000000000000000000, 0.000000000000000000 ) ) ;
#25076=ORIENTED_EDGE ( 'NONE', *, *, #51542, .T. ) ;
#25085=CARTESIAN_POINT ( 'NONE',  ( 6.239160159721271803, 2.500000000000000000, -3.193457606803198789 ) ) ;
#25093=VERTEX_POINT ( 'NONE', #274 ) ;
#25286=ADVANCED_BREP_SHAPE_REPRESENTATION ( '', ( #50051, #42840 ), #1086 ) ;
#25296=CARTESIAN_POINT ( 'NONE',  ( -4.041451884327378785, 1.417096231345241542, 7.000000000000000000 ) ) ;
#25415=EDGE_CURVE ( 'NONE', #37645, #39091, #13662, .T. ) ;
#25436=ORIENTED_EDGE ( 'NONE', *, *, #49443, .F. ) ;
#25446=CARTESIAN_POINT ( 'NONE',  ( -6.418790567836330396, 2.472216779103305395, 2.882328613363590808 ) ) ;
#25505=ORIENTED_EDGE ( 'NONE', *, *, #64872, .T. ) ;
#25569=ADVANCED_FACE ( 'NONE', ( #24721 ), #51944, .T. ) ;
#25695=LINE ( 'NONE', #21124, #38327 ) ;
#25729=ORIENTED_EDGE ( 'NONE', *, *, #55980, .F. ) ;
#25818=VERTEX_POINT ( 'NONE', #53563 ) ;
#25900=CARTESIAN_POINT ( 'NONE',  ( 2.418047948276647041, -2.101261491285135286, -7.000000000000002665 ) ) ;
#26010=CARTESIAN_POINT ( 'NONE',  ( -8.082903768654761123, 2.500000000000000000, -1.781658826789683271E-15 ) ) ;
#26320=CONICAL_SURFACE ( 'NONE', #13984, 3.000000000000000444, 0.7853981633974517207 ) ;
#26345=CARTESIAN_POINT ( 'NONE',  ( 6.759171781091399822, 2.392512705203733603, 2.292771058063876488 ) ) ;
#26652=CARTESIAN_POINT ( 'NONE',  ( 7.441974819423174736, -2.003239292658530513, -1.110121504110836987 ) ) ;
#26700=CONICAL_SURFACE ( 'NONE', #51430, 3.000000000000000444, 0.7853981633974517207 ) ;
#26713=CARTESIAN_POINT ( 'NONE',  ( -4.357963766315032572, 1.733608113333017453, 6.451785339198141678 ) ) ;
#26863=CARTESIAN_POINT ( 'NONE',  ( 0.000000000000000000, 2.500000000000000000, 0.000000000000000000 ) ) ;
#26912=FACE_OUTER_BOUND ( 'NONE', #50201, .T. ) ;
#26965=CARTESIAN_POINT ( 'NONE',  ( 0.000000000000000000, -2.500000000000000000, 0.000000000000000000 ) ) ;
#27143=CONICAL_SURFACE ( 'NONE', #54112, 6.999999999999997335, 0.7853981633974500554 ) ;
#27288=ORIENTED_EDGE ( 'NONE', *, *, #12983, .T. ) ;
#27379=CARTESIAN_POINT ( 'NONE',  ( 5.185928986913072691, 2.291132984336067935, 5.017707510222361833 ) ) ;
#27405=ORIENTED_EDGE ( 'NONE', *, *, #14888, .F. ) ;
#27707=ORIENTED_EDGE ( 'NONE', *, *, #12199, .F. ) ;
#27765=CARTESIAN_POINT ( 'NONE',  ( -5.185928986913076244, 2.291132984336064382, -5.017707510222360057 ) ) ;
#27937=DIRECTION ( 'NONE',  ( 0.8660254037844387076, -0.000000000000000000, 0.4999999999999998890 ) ) ;
#28099=B_SPLINE_CURVE_WITH_KNOTS ( 'NONE', 3,
 ( #46936, #35644, #40945, #62365, #30682, #20496 ),
 .UNSPECIFIED., .F., .F.,
 ( 4, 2, 4 ),
 ( 0.004189585287972440175, 0.006269578072783811573, 0.008349570857595182971 ),
 .UNSPECIFIED. ) ;
#28153=AXIS2_PLACEMENT_3D ( 'NONE', #65692, #23462, #60400 ) ;
#28295=CONICAL_SURFACE ( 'NONE', #65444, 3.499999999999997780, 0.7853981633974452814 ) ;
#28429=CARTESIAN_POINT ( 'NONE',  ( -0.3558155366086588334, -2.493171897977409568, 7.000000000000000000 ) ) ;
#28517=VERTEX_POINT ( 'NONE', #9797 ) ;
#28522=CARTESIAN_POINT ( 'NONE',  ( 6.062177826491068622, 2.500000000000000000, -3.500000000000001332 ) ) ;
#28574=ADVANCED_FACE ( 'NONE', ( #53044 ), #27143, .T. ) ;
#28712=ORIENTED_EDGE ( 'NONE', *, *, #65025, .F. ) ;
#28976=B_SPLINE_CURVE_WITH_KNOTS ( 'NONE', 3,
 ( #69382, #69038, #42349, #63736, #64086, #15939 ),
 .UNSPECIFIED., .F., .F.,
 ( 4, 2, 4 ),
 ( 0.004189585287972440175, 0.006269578072783815043, 0.008349570857595189910 ),
 .UNSPECIFIED. ) ;
#29013=B_SPLINE_CURVE_WITH_KNOTS ( 'NONE', 3,
 ( #35224, #51401, #10572, #64374, #26713, #43329 ),
 .UNSPECIFIED., .F., .F.,
 ( 4, 2, 4 ),
 ( 0.004189585287972438440, 0.006269578072783812440, 0.008349570857595186441 ),
 .UNSPECIFIED. ) ;
#29019=AXIS2_PLACEMENT_3D ( 'NONE', #43666, #45048, #17607 ) ;
#29093=ORIENTED_EDGE ( 'NONE', *, *, #55202, .T. ) ;
#29129=DIRECTION ( 'NONE',  ( 0.000000000000000000, 1.000000000000000000, 0.000000000000000000 ) ) ;
#29301=DIRECTION ( 'NONE',  ( 0.000000000000000000, 0.000000000000000000, 1.000000000000000000 ) ) ;
#29377=ORIENTED_EDGE ( 'NONE', *, *, #19280, .T. ) ;
#29404=CARTESIAN_POINT ( 'NONE',  ( -1.233556390955557802, 2.406758536254373748, 6.999999999999999112 ) ) ;
#29431=CARTESIAN_POINT ( 'NONE',  ( 0.000000000000000000, 2.000000000000000444, 0.000000000000000000 ) ) ;
#29484=DIRECTION ( 'NONE',  ( 0.000000000000000000, 0.000000000000000000, 1.000000000000000000 ) ) ;
#29495=CARTESIAN_POINT ( 'NONE',  ( -3.414270897520784942, -1.730686724748536465, 7.000000000000000000 ) ) ;
#29501=CARTESIAN_POINT ( 'NONE',  ( 6.413663052920311358, -2.499999999999998668, 2.891209729714698806 ) ) ;
#29543=CARTESIAN_POINT ( 'NONE',  ( 2.418047948263831071, 2.101261491288920702, 7.000000000000001776 ) ) ;
#29760=CARTESIAN_POINT ( 'NONE',  ( 3.409440450227775532, -1.719598803868653603, 7.000000000000000888 ) ) ;
#29890=EDGE_LOOP ( 'NONE', ( #24337, #13300, #22045, #6140, #20894, #65378 ) ) ;
#30142=VERTEX_POINT ( 'NONE', #23315 ) ;
#30149=VERTEX_POINT ( 'NONE', #745 ) ;
#30236=PLANE ( 'NONE',  #65813 ) ;
#30241=AXIS2_PLACEMENT_3D ( 'NONE', #64941, #54725, #43892 ) ;
#30308=STYLED_ITEM ( 'NONE', ( #65441 ), #25286 ) ;
#30454=DIRECTION ( 'NONE',  ( 0.000000000000000000, 1.000000000000000000, 0.000000000000000000 ) ) ;
#30495=VERTEX_POINT ( 'NONE', #12666 ) ;
#30502=EDGE_LOOP ( 'NONE', ( #67384, #21759, #31471, #59150, #14076, #738 ) ) ;
#30663=DIRECTION ( 'NONE',  ( -0.8660254037844384856, 0.000000000000000000, 0.5000000000000004441 ) ) ;
#30682=CARTESIAN_POINT ( 'NONE',  ( -7.766391886667105560, -1.733608113333017453, -0.5482146608018624301 ) ) ;
#30914=B_SPLINE_CURVE_WITH_KNOTS ( 'NONE', 3,
 ( #308, #64748, #16589, #27765, #17938, #12648, #11965, #12999 ),
 .UNSPECIFIED., .F., .F.,
 ( 4, 2, 2, 4 ),
 ( 2.544316211733585141E-07, 0.002094919859796805575, 0.003142252573884622441, 0.004189585287972440175 ),
 .UNSPECIFIED. ) ;
#30968=ORIENTED_EDGE ( 'NONE', *, *, #6575, .T. ) ;
#30973=ORIENTED_EDGE ( 'NONE', *, *, #39165, .T. ) ;
#31049=DIRECTION ( 'NONE',  ( -0.000000000000000000, 1.000000000000000000, -0.000000000000000000 ) ) ;
#31055=CARTESIAN_POINT ( 'NONE',  ( 0.000000000000000000, 2.500000000000000000, 0.000000000000000000 ) ) ;
#31236=DIRECTION ( 'NONE',  ( -0.000000000000000000, -1.000000000000000000, -0.000000000000000000 ) ) ;
#31263=ORIENTED_EDGE ( 'NONE', *, *, #68796, .F. ) ;
#31285=FACE_OUTER_BOUND ( 'NONE', #29890, .T. ) ;
#31336=DIRECTION ( 'NONE',  ( 1.776356839400250465E-15, 0.000000000000000000, 1.000000000000000000 ) ) ;
#31368=CARTESIAN_POINT ( 'NONE',  ( -4.041451884327380562, 2.500000000000000000, -7.000000000000003553 ) ) ;
#31392=EDGE_CURVE ( 'NONE', #12794, #38350, #48250, .T. ) ;
#31430=ORIENTED_EDGE ( 'NONE', *, *, #39762, .T. ) ;
#31440=ORIENTED_EDGE ( 'NONE', *, *, #50357, .F. ) ;
#31471=ORIENTED_EDGE ( 'NONE', *, *, #65674, .T. ) ;
#31472=PLANE ( 'NONE',  #2083 ) ;
#31497=CARTESIAN_POINT ( 'NONE',  ( 0.000000000000000000, 2.000000000000000444, 3.000000000000000444 ) ) ;
#31509=AXIS2_PLACEMENT_3D ( 'NONE', #8181, #40201, #7812 ) ;
#31598=CARTESIAN_POINT ( 'NONE',  ( -1.745454270680677045, -2.292880170256994976, -7.000000000000003553 ) ) ;
#31824=DIRECTION ( 'NONE',  ( 0.000000000000000000, 1.000000000000000000, 0.000000000000000000 ) ) ;
#31968=DIRECTION ( 'NONE',  ( -8.881784197001252323E-16, 0.000000000000000000, 1.000000000000000000 ) ) ;
#32031=EDGE_CURVE ( 'NONE', #39091, #30142, #7374, .T. ) ;
#32110=CARTESIAN_POINT ( 'NONE',  ( 6.062177826491068622, -2.500000000000000000, -3.500000000000001332 ) ) ;
#32137=CARTESIAN_POINT ( 'NONE',  ( 4.041451884327375232, 1.417096231345241097, -7.000000000000002665 ) ) ;
#32292=CARTESIAN_POINT ( 'NONE',  ( -3.414270897523328241, -1.730686724747262373, -7.000000000000004441 ) ) ;
#32295=CARTESIAN_POINT ( 'NONE',  ( 6.767634268437461742, -2.367558512213881805, -2.278113600022080298 ) ) ;
#32356=ORIENTED_EDGE ( 'NONE', *, *, #25415, .T. ) ;
#32374=ORIENTED_EDGE ( 'NONE', *, *, #34069, .T. ) ;
#32377=CARTESIAN_POINT ( 'NONE',  ( 5.885195493260862776, -2.499999999999998668, 3.806542393196804763 ) ) ;
#32401=CONICAL_SURFACE ( 'NONE', #29019, 6.999999999999997335, 0.7853981633974500554 ) ;
#32419=CARTESIAN_POINT ( 'NONE',  ( 0.000000000000000000, -2.500000000000000000, 0.000000000000000000 ) ) ;
#32449=ADVANCED_FACE ( 'NONE', ( #12827 ), #65606, .F. ) ;
#32514=CARTESIAN_POINT ( 'NONE',  ( 4.286263797015733637E-16, -2.500000000000000000, 3.499999999999997780 ) ) ;
#32610=ORIENTED_EDGE ( 'NONE', *, *, #66650, .F. ) ;
#32657=CARTESIAN_POINT ( 'NONE',  ( -6.239160159721276244, -2.499999999999999556, 3.193457606803197013 ) ) ;
#32666=EDGE_LOOP ( 'NONE', ( #6001, #61834, #61921 ) ) ;
#32729=( NAMED_UNIT ( * ) SI_UNIT ( $, .STERADIAN. ) SOLID_ANGLE_UNIT ( ) );
#32740=DIRECTION ( 'NONE',  ( 0.000000000000000000, 0.000000000000000000, 1.000000000000000000 ) ) ;
#32764=CIRCLE ( 'NONE', #58620, 3.000000000000000444 ) ;
#32879=CLOSED_SHELL ( 'NONE', ( #16257, #38317, #21206, #35995, #38965, #9053, #32449, #40978, #58154, #10459, #43432, #28574, #15221, #60574, #48411, #4656, #68327, #1675, #8192, #66485, #59832, #25569, #24445, #18272, #13893, #24770 ) ) ;
#32904=DIRECTION ( 'NONE',  ( 8.659560562354906974E-17, -0.7071067811865496822, 0.7071067811865453523 ) ) ;
#32943=CARTESIAN_POINT ( 'NONE',  ( -5.185928986913076244, -2.291132984336064382, -5.017707510222360057 ) ) ;
#33002=CARTESIAN_POINT ( 'NONE',  ( 6.938426666069061000, -2.291132984336068823, -1.982292489777642164 ) ) ;
#33107=DIRECTION ( 'NONE',  ( 0.000000000000000000, 0.000000000000000000, 1.000000000000000000 ) ) ;
#33181=ORIENTED_EDGE ( 'NONE', *, *, #43175, .T. ) ;
#33285=CARTESIAN_POINT ( 'NONE',  ( -4.041451884327380562, -1.417096231345237545, -7.000000000000003553 ) ) ;
#33351=CIRCLE ( 'NONE', #16574, 3.500000000000003553 ) ;
#33610=CARTESIAN_POINT ( 'NONE',  ( 0.000000000000000000, 2.500000000000000000, 0.000000000000000000 ) ) ;
#33767=( NAMED_UNIT ( * ) PLANE_ANGLE_UNIT ( ) SI_UNIT ( $, .RADIAN. ) );
#33839=EDGE_CURVE ( 'NONE', #30495, #58318, #35907, .T. ) ;
#33884=CARTESIAN_POINT ( 'NONE',  ( 8.082903768654761123, -1.417096231345241097, 9.294316082458970795E-16 ) ) ;
#33892=ORIENTED_EDGE ( 'NONE', *, *, #50796, .F. ) ;
#34069=EDGE_CURVE ( 'NONE', #52109, #42774, #1068, .T. ) ;
#34261=DIRECTION ( 'NONE',  ( 0.000000000000000000, 0.000000000000000000, 1.000000000000000000 ) ) ;
#34303=CARTESIAN_POINT ( 'NONE',  ( 0.000000000000000000, -2.500000000000000000, -3.499999999999997780 ) ) ;
#34311=CARTESIAN_POINT ( 'NONE',  ( 4.041451884327375232, 2.500000000000000000, -7.000000000000002665 ) ) ;
#34321=VERTEX_POINT ( 'NONE', #55587 ) ;
#34327=CIRCLE ( 'NONE', #66925, 3.500000000000003553 ) ;
#34383=EDGE_CURVE ( 'NONE', #63907, #10734, #18917, .T. ) ;
#34395=EDGE_LOOP ( 'NONE', ( #66907, #25076, #12400, #57640, #23172, #52115 ) ) ;
#34435=FACE_OUTER_BOUND ( 'NONE', #32666, .T. ) ;
#34846=CARTESIAN_POINT ( 'NONE',  ( 0.000000000000000000, 2.500000000000000000, 0.000000000000000000 ) ) ;
#34856=( GEOMETRIC_REPRESENTATION_CONTEXT ( 3 ) GLOBAL_UNCERTAINTY_ASSIGNED_CONTEXT ( ( #50148 ) ) GLOBAL_UNIT_ASSIGNED_CONTEXT ( ( #17944, #33767, #32729 ) ) REPRESENTATION_CONTEXT ( 'NONE', 'WORKASPACE' ) );
#34992=DIRECTION ( 'NONE',  ( 0.000000000000000000, 0.000000000000000000, 1.000000000000000000 ) ) ;
#35159=ORIENTED_EDGE ( 'NONE', *, *, #31392, .F. ) ;
#35224=CARTESIAN_POINT ( 'NONE',  ( -6.062177826491069510, 2.500000000000000000, 3.499999999999999556 ) ) ;
#35310=CARTESIAN_POINT ( 'NONE',  ( 0.000000000000000000, -2.500000000000000000, 0.000000000000000000 ) ) ;
#35329=CIRCLE ( 'NONE', #39876, 3.000000000000000444 ) ;
#35395=CARTESIAN_POINT ( 'NONE',  ( 3.728455551739337626, -1.573594397639262343, 6.999999999999999112 ) ) ;
#35493=AXIS2_PLACEMENT_3D ( 'NONE', #48670, #59157, #16978 ) ;
#35612=B_SPLINE_CURVE_WITH_KNOTS ( 'NONE', 3,
 ( #7277, #8325, #45290, #18524, #29404, #61070, #39309, #24462, #51565 ),
 .UNSPECIFIED., .F., .F.,
 ( 4, 2, 1, 2, 4 ),
 ( 0.007659788818331629730, 0.009746199297478887538, 0.01078940453705251601, 0.01131100715683933111, 0.01183260977662614448 ),
 .UNSPECIFIED. ) ;
#35644=CARTESIAN_POINT ( 'NONE',  ( -6.413663052920317575, -2.499999999999997780, -2.891209729714699250 ) ) ;
#35671=CARTESIAN_POINT ( 'NONE',  ( -7.766025168014157209, 1.733974831985841458, 0.5488498361408482573 ) ) ;
#35732=ORIENTED_EDGE ( 'NONE', *, *, #25415, .F. ) ;
#35780=CARTESIAN_POINT ( 'NONE',  ( 4.041451884327375232, -1.417096231345241097, -7.000000000000002665 ) ) ;
#35902=AXIS2_PLACEMENT_3D ( 'NONE', #60360, #17816, #43214 ) ;
#35907=CIRCLE ( 'NONE', #16841, 6.999999999999997335 ) ;
#35932=ORIENTED_EDGE ( 'NONE', *, *, #34069, .F. ) ;
#35985=PRESENTATION_STYLE_ASSIGNMENT (( #4994 ) ) ;
#35995=ADVANCED_FACE ( 'NONE', ( #66886 ), #3132, .F. ) ;
#36050=EDGE_CURVE ( 'NONE', #30149, #52109, #24296, .T. ) ;
#36280=DIRECTION ( 'NONE',  ( 0.000000000000000000, 0.000000000000000000, 1.000000000000000000 ) ) ;
#36331=DIRECTION ( 'NONE',  ( -0.000000000000000000, -1.000000000000000000, -0.000000000000000000 ) ) ;
#36336=CARTESIAN_POINT ( 'NONE',  ( 5.185928986913072691, -2.291132984336067935, 5.017707510222361833 ) ) ;
#36388=DIRECTION ( 'NONE',  ( 0.000000000000000000, 0.000000000000000000, 1.000000000000000000 ) ) ;
#36463=CARTESIAN_POINT ( 'NONE',  ( 4.041451884327377897, 1.417096231345241319, 7.000000000000000888 ) ) ;
#36472=CONICAL_SURFACE ( 'NONE', #21823, 6.999999999999997335, 0.7853981633974500554 ) ;
#36499=EDGE_CURVE ( 'NONE', #30149, #13760, #67832, .T. ) ;
#36592=CIRCLE ( 'NONE', #53420, 3.499999999999997780 ) ;
#36696=CARTESIAN_POINT ( 'NONE',  ( 4.358330484967978258, -1.733974831985841458, 6.451150163859151299 ) ) ;
#36717=ORIENTED_EDGE ( 'NONE', *, *, #10579, .T. ) ;
#36719=SURFACE_SIDE_STYLE ('',( #58470 ) ) ;
#36806=EDGE_CURVE ( 'NONE', #51506, #63065, #43223, .T. ) ;
#36929=CARTESIAN_POINT ( 'NONE',  ( 6.062177826491068622, -2.500000000000000000, -3.500000000000001332 ) ) ;
#37056=( NAMED_UNIT ( * ) SI_UNIT ( $, .STERADIAN. ) SOLID_ANGLE_UNIT ( ) );
#37069=APPLICATION_CONTEXT ( 'automotive_design' ) ;
#37114=EDGE_LOOP ( 'NONE', ( #47170, #46840, #53871 ) ) ;
#37217=ORIENTED_EDGE ( 'NONE', *, *, #62179, .F. ) ;
#37242=CARTESIAN_POINT ( 'NONE',  ( -8.082903768654761123, -1.417096231345241097, -1.759977097422839922E-15 ) ) ;
#37285=PRODUCT_DEFINITION_SHAPE ( 'NONE', 'NONE',  #43868 ) ;
#37448=EDGE_CURVE ( 'NONE', #25818, #67895, #22993, .T. ) ;
#37645=VERTEX_POINT ( 'NONE', #32137 ) ;
#37670=CARTESIAN_POINT ( 'NONE',  ( 4.682380833558961619, 2.003239292658529624, 5.889878495889163901 ) ) ;
#37673=FACE_OUTER_BOUND ( 'NONE', #44384, .T. ) ;
#37724=DIRECTION ( 'NONE',  ( -0.000000000000000000, -1.000000000000000000, -0.000000000000000000 ) ) ;
#37749=DIRECTION ( 'NONE',  ( 0.000000000000000000, 0.000000000000000000, 1.000000000000000000 ) ) ;
#38050=SURFACE_STYLE_FILL_AREA ( #48960 ) ;
#38053=AXIS2_PLACEMENT_3D ( 'NONE', #40951, #23689, #29301 ) ;
#38213=EDGE_CURVE ( 'NONE', #25093, #49290, #38851, .T. ) ;
#38316=CARTESIAN_POINT ( 'NONE',  ( 6.239160159721271803, -2.500000000000000000, -3.193457606803198789 ) ) ;
#38317=ADVANCED_FACE ( 'NONE', ( #65081 ), #26320, .F. ) ;
#38327=VECTOR ( 'NONE', #42625, 1000.000000000000000 ) ;
#38350=VERTEX_POINT ( 'NONE', #41178 ) ;
#38550=CARTESIAN_POINT ( 'NONE',  ( 3.728455551740339047, 1.573594397638760300, -7.000000000000004441 ) ) ;
#38690=CARTESIAN_POINT ( 'NONE',  ( -6.418790567836330396, -2.472216779103305395, 2.882328613363590808 ) ) ;
#38754=SURFACE_SIDE_STYLE ('',( #38050 ) ) ;
#38769=ORIENTED_EDGE ( 'NONE', *, *, #43175, .F. ) ;
#38785=CARTESIAN_POINT ( 'NONE',  ( 3.673940397442060361E-16, 2.000000000000000444, -3.000000000000000444 ) ) ;
#38817=DIRECTION ( 'NONE',  ( 0.000000000000000000, 0.000000000000000000, 1.000000000000000000 ) ) ;
#38851=B_SPLINE_CURVE_WITH_KNOTS ( 'NONE', 3,
 ( #21494, #36696, #43005, #36336, #58113, #57763, #32377, #63017 ),
 .UNSPECIFIED., .F., .F.,
 ( 4, 2, 2, 4 ),
 ( 2.544316211733585141E-07, 0.002094919859796804708, 0.003142252573884620707, 0.004189585287972436706 ),
 .UNSPECIFIED. ) ;
#38924=PRODUCT_DEFINITION_CONTEXT ( 'detailed design', #16811, 'design' ) ;
#38938=DIRECTION ( 'NONE',  ( 0.000000000000000000, -1.000000000000000000, 0.000000000000000000 ) ) ;
#38959=ORIENTED_EDGE ( 'NONE', *, *, #12983, .F. ) ;
#38965=ADVANCED_FACE ( 'NONE', ( #57061 ), #67624, .F. ) ;
#39091=VERTEX_POINT ( 'NONE', #41609 ) ;
#39165=EDGE_CURVE ( 'NONE', #42774, #52109, #36592, .T. ) ;
#39298=B_SPLINE_CURVE_WITH_KNOTS ( 'NONE', 3,
 ( #44936, #19541, #12878, #8317, #7270, #29760, #35395, #14274 ),
 .UNSPECIFIED., .F., .F.,
 ( 4, 2, 2, 4 ),
 ( 0.01183260977662614621, 0.01392219916432753737, 0.01496699385817823122, 0.01601178855202892506 ),
 .UNSPECIFIED. ) ;
#39309=CARTESIAN_POINT ( 'NONE',  ( -0.3558155366086579452, 2.493171897977409568, 7.000000000000000000 ) ) ;
#39396=CARTESIAN_POINT ( 'NONE',  ( -2.754976799258605169, -2.005084411322475724, 7.000000000000000000 ) ) ;
#39516=CIRCLE ( 'NONE', #2298, 6.999999999999997335 ) ;
#39550=AXIS2_PLACEMENT_3D ( 'NONE', #68709, #31049, #36388 ) ;
#39579=EDGE_CURVE ( 'NONE', #34321, #40436, #40443, .T. ) ;
#39641=VECTOR ( 'NONE', #40337, 1000.000000000000000 ) ;
#39742=CARTESIAN_POINT ( 'NONE',  ( -1.233556390955556914, -2.406758536254373748, 6.999999999999999112 ) ) ;
#39743=ORIENTED_EDGE ( 'NONE', *, *, #60204, .F. ) ;
#39756=EDGE_CURVE ( 'NONE', #34321, #3748, #56872, .T. ) ;
#39762=EDGE_CURVE ( 'NONE', #4242, #51146, #53870, .T. ) ;
#39876=AXIS2_PLACEMENT_3D ( 'NONE', #57145, #62762, #40661 ) ;
#40097=CARTESIAN_POINT ( 'NONE',  ( 0.000000000000000000, -2.500000000000000000, 0.000000000000000000 ) ) ;
#40201=DIRECTION ( 'NONE',  ( -0.000000000000000000, 1.000000000000000000, -0.000000000000000000 ) ) ;
#40337=DIRECTION ( 'NONE',  ( -0.000000000000000000, 1.000000000000000000, -0.000000000000000000 ) ) ;
#40436=VERTEX_POINT ( 'NONE', #20210 ) ;
#40443=B_SPLINE_CURVE_WITH_KNOTS ( 'NONE', 3,
 ( #9515, #69607, #26345, #10187, #52763, #43293 ),
 .UNSPECIFIED., .F., .F.,
 ( 4, 2, 4 ),
 ( 0.004189585287972436706, 0.006269578072783809838, 0.008349570857595182971 ),
 .UNSPECIFIED. ) ;
#40613=DIRECTION ( 'NONE',  ( 0.000000000000000000, 0.000000000000000000, 1.000000000000000000 ) ) ;
#40619=EDGE_CURVE ( 'NONE', #28517, #41509, #7079, .T. ) ;
#40661=DIRECTION ( 'NONE',  ( 0.000000000000000000, 0.000000000000000000, 1.000000000000000000 ) ) ;
#40783=CARTESIAN_POINT ( 'NONE',  ( 6.062177826491067734, -2.500000000000000000, 3.500000000000000000 ) ) ;
#40824=ORIENTED_EDGE ( 'NONE', *, *, #33839, .T. ) ;
#40943=VECTOR ( 'NONE', #5859, 1000.000000000000000 ) ;
#40945=CARTESIAN_POINT ( 'NONE',  ( -6.759171781091400710, -2.392512705203732715, -2.292771058063876488 ) ) ;
#40951=CARTESIAN_POINT ( 'NONE',  ( 0.000000000000000000, -1.999999999999999556, 0.000000000000000000 ) ) ;
#40973=CARTESIAN_POINT ( 'NONE',  ( 0.000000000000000000, -2.500000000000000000, 0.000000000000000000 ) ) ;
#40978=ADVANCED_FACE ( 'NONE', ( #37673 ), #21794, .F. ) ;
#41178=CARTESIAN_POINT ( 'NONE',  ( 0.000000000000000000, 2.500000000000000000, 3.500000000000003553 ) ) ;
#41186=ORIENTED_EDGE ( 'NONE', *, *, #55202, .F. ) ;
#41214=CARTESIAN_POINT ( 'NONE',  ( 4.041451884327377897, 2.500000000000000000, 7.000000000000000888 ) ) ;
#41231=EDGE_LOOP ( 'NONE', ( #36717, #29093, #7376, #66240, #4906, #12203 ) ) ;
#41509=VERTEX_POINT ( 'NONE', #10396 ) ;
#41516=CARTESIAN_POINT ( 'NONE',  ( -7.511572993685801073E-16, 2.500000000000000000, 7.000000000000000888 ) ) ;
#41538=DIRECTION ( 'NONE',  ( -1.000000000000000000, 0.000000000000000000, -1.073081856240828689E-16 ) ) ;
#41598=AXIS2_PLACEMENT_3D ( 'NONE', #3545, #25049, #14861 ) ;
#41609=CARTESIAN_POINT ( 'NONE',  ( 7.511572993685799101E-16, 2.500000000000000000, -6.999999999999997335 ) ) ;
#41732=CARTESIAN_POINT ( 'NONE',  ( 0.000000000000000000, 2.500000000000000000, 0.000000000000000000 ) ) ;
#41751=AXIS2_PLACEMENT_3D ( 'NONE', #60156, #57296, #19666 ) ;
#41907=DIRECTION ( 'NONE',  ( 1.073081856240828689E-16, 0.000000000000000000, -1.000000000000000000 ) ) ;
#42348=DIRECTION ( 'NONE',  ( -0.000000000000000000, -1.000000000000000000, -0.000000000000000000 ) ) ;
#42349=CARTESIAN_POINT ( 'NONE',  ( 5.365183871890737421, 2.392512705203734935, -4.707228941936126176 ) ) ;
#42439=DIRECTION ( 'NONE',  ( 0.000000000000000000, 1.000000000000000000, 0.000000000000000000 ) ) ;
#42625=DIRECTION ( 'NONE',  ( -0.000000000000000000, 1.000000000000000000, -0.000000000000000000 ) ) ;
#42687=B_SPLINE_CURVE_WITH_KNOTS ( 'NONE', 3,
 ( #43224, #1226, #44252, #22756, #6911, #55448 ),
 .UNSPECIFIED., .F., .F.,
 ( 4, 2, 4 ),
 ( 0.004189585287972438440, 0.006269578072783812440, 0.008349570857595186441 ),
 .UNSPECIFIED. ) ;
#42774=VERTEX_POINT ( 'NONE', #32514 ) ;
#42840=AXIS2_PLACEMENT_3D ( 'NONE', #59977, #7217, #49786 ) ;
#43005=CARTESIAN_POINT ( 'NONE',  ( 4.682380833558961619, -2.003239292658529624, 5.889878495889163901 ) ) ;
#43175=EDGE_CURVE ( 'NONE', #6283, #51146, #8930, .T. ) ;
#43214=DIRECTION ( 'NONE',  ( 0.000000000000000000, 0.000000000000000000, 1.000000000000000000 ) ) ;
#43223=LINE ( 'NONE', #64627, #40943 ) ;
#43224=CARTESIAN_POINT ( 'NONE',  ( -6.062177826491069510, -2.500000000000000000, 3.499999999999999556 ) ) ;
#43264=ORIENTED_EDGE ( 'NONE', *, *, #68796, .T. ) ;
#43286=ORIENTED_EDGE ( 'NONE', *, *, #36499, .T. ) ;
#43293=CARTESIAN_POINT ( 'NONE',  ( 8.082903768654761123, 1.417096231345241097, 9.294316082458970795E-16 ) ) ;
#43307=DIRECTION ( 'NONE',  ( -0.4999999999999999445, 0.000000000000000000, -0.8660254037844385966 ) ) ;
#43329=CARTESIAN_POINT ( 'NONE',  ( -4.041451884327378785, 1.417096231345241542, 7.000000000000000000 ) ) ;
#43360=SURFACE_STYLE_USAGE ( .BOTH. , #38754 ) ;
#43413=ORIENTED_EDGE ( 'NONE', *, *, #53541, .T. ) ;
#43432=ADVANCED_FACE ( 'NONE', ( #966 ), #32401, .T. ) ;
#43526=LINE ( 'NONE', #10433, #20225 ) ;
#43540=CARTESIAN_POINT ( 'NONE',  ( -5.356721384544675502, -2.367558512213879141, -4.721886399977922366 ) ) ;
#43666=CARTESIAN_POINT ( 'NONE',  ( 0.000000000000000000, 2.500000000000000000, 0.000000000000000000 ) ) ;
#43777=ORIENTED_EDGE ( 'NONE', *, *, #51542, .F. ) ;
#43835=CONICAL_SURFACE ( 'NONE', #19064, 6.999999999999997335, 0.7853981633974500554 ) ;
#43868=PRODUCT_DEFINITION ( 'UNKNOWN', '', #66328, #38924 ) ;
#43892=DIRECTION ( 'NONE',  ( 0.000000000000000000, 0.000000000000000000, 1.000000000000000000 ) ) ;
#44132=DIRECTION ( 'NONE',  ( 0.000000000000000000, 0.000000000000000000, 1.000000000000000000 ) ) ;
#44147=ORIENTED_EDGE ( 'NONE', *, *, #59279, .F. ) ;
#44252=CARTESIAN_POINT ( 'NONE',  ( -5.365183871890740974, -2.392512705203733159, 4.707228941936125288 ) ) ;
#44291=CARTESIAN_POINT ( 'NONE',  ( 0.000000000000000000, -1.999999999999999556, 3.000000000000000444 ) ) ;
#44311=CARTESIAN_POINT ( 'NONE',  ( 0.000000000000000000, -2.500000000000000000, 0.000000000000000000 ) ) ;
#44384=EDGE_LOOP ( 'NONE', ( #15518, #31430, #25505, #878, #14854, #27405 ) ) ;
#44387=( NAMED_UNIT ( * ) SI_UNIT ( $, .STERADIAN. ) SOLID_ANGLE_UNIT ( ) );
#44597=STYLED_ITEM ( 'NONE', ( #35985 ), #50051 ) ;
#44630=CARTESIAN_POINT ( 'NONE',  ( -2.754976799268631815, 2.005084411318701409, -7.000000000000003553 ) ) ;
#44925=EDGE_CURVE ( 'NONE', #40436, #24428, #53425, .T. ) ;
#44936=CARTESIAN_POINT ( 'NONE',  ( -7.511572993685798115E-16, -2.500000000000000000, 6.999999999999997335 ) ) ;
#45048=DIRECTION ( 'NONE',  ( 0.000000000000000000, -1.000000000000000000, 0.000000000000000000 ) ) ;
#45111=DIRECTION ( 'NONE',  ( -0.8660254037844385966, 0.000000000000000000, -0.5000000000000003331 ) ) ;
#45201=DIRECTION ( 'NONE',  ( 0.000000000000000000, 1.000000000000000000, 0.000000000000000000 ) ) ;
#45290=CARTESIAN_POINT ( 'NONE',  ( -2.754976799258605169, 2.005084411322475280, 7.000000000000000000 ) ) ;
#45333=EDGE_LOOP ( 'NONE', ( #11984, #65945, #4161 ) ) ;
#45379=CARTESIAN_POINT ( 'NONE',  ( -0.1770589935948743143, -2.499999999999996891, 7.000000000000002665 ) ) ;
#45467=DIRECTION ( 'NONE',  ( -0.5000000000000002220, 0.000000000000000000, 0.8660254037844384856 ) ) ;
#45750=VERTEX_POINT ( 'NONE', #14253 ) ;
#45761=CARTESIAN_POINT ( 'NONE',  ( 1.400957079539663752, 2.390838073342431258, 7.000000000000000000 ) ) ;
#45816=DIRECTION ( 'NONE',  ( 0.000000000000000000, 0.000000000000000000, 1.000000000000000000 ) ) ;
#45866=CARTESIAN_POINT ( 'NONE',  ( 7.441974819423174736, 2.003239292658530513, -1.110121504110836987 ) ) ;
#46014=AXIS2_PLACEMENT_3D ( 'NONE', #31055, #2895, #14911 ) ;
#46096=EDGE_CURVE ( 'NONE', #3748, #37645, #28976, .T. ) ;
#46232=CARTESIAN_POINT ( 'NONE',  ( 7.766025168014159874, 1.733974831985843013, -0.5488498361408489234 ) ) ;
#46619=CARTESIAN_POINT ( 'NONE',  ( -6.938426666069064552, 2.291132984336068379, 1.982292489777641720 ) ) ;
#46840=ORIENTED_EDGE ( 'NONE', *, *, #50754, .T. ) ;
#46844=ORIENTED_EDGE ( 'NONE', *, *, #58146, .F. ) ;
#46936=CARTESIAN_POINT ( 'NONE',  ( -6.062177826491070398, -2.500000000000000000, -3.499999999999998224 ) ) ;
#47112=EDGE_LOOP ( 'NONE', ( #14917, #43777, #11977 ) ) ;
#47170=ORIENTED_EDGE ( 'NONE', *, *, #39579, .T. ) ;
#47460=CARTESIAN_POINT ( 'NONE',  ( 1.400957079523476700, 2.390838073347306914, -7.000000000000002665 ) ) ;
#47499=CARTESIAN_POINT ( 'NONE',  ( -0.1770589935874667675, -2.499999999999994671, -7.000000000000002665 ) ) ;
#47604=ORIENTED_EDGE ( 'NONE', *, *, #16575, .F. ) ;
#47631=LINE ( 'NONE', #31368, #65892 ) ;
#47865=EDGE_CURVE ( 'NONE', #51506, #63907, #35612, .T. ) ;
#47994=FACE_OUTER_BOUND ( 'NONE', #13533, .T. ) ;
#48193=CONICAL_SURFACE ( 'NONE', #6549, 6.999999999999997335, 0.7853981633974500554 ) ;
#48250=LINE ( 'NONE', #59434, #62307 ) ;
#48256=DIRECTION ( 'NONE',  ( 0.000000000000000000, 0.000000000000000000, -1.000000000000000000 ) ) ;
#48276=CARTESIAN_POINT ( 'NONE',  ( 0.000000000000000000, -2.500000000000000000, 0.000000000000000000 ) ) ;
#48314=FACE_OUTER_BOUND ( 'NONE', #47112, .T. ) ;
#48411=ADVANCED_FACE ( 'NONE', ( #26912 ), #36472, .T. ) ;
#48521=CARTESIAN_POINT ( 'NONE',  ( -2.754976799268632703, -2.005084411318700077, -7.000000000000003553 ) ) ;
#48542=DIRECTION ( 'NONE',  ( -0.000000000000000000, -1.000000000000000000, -0.000000000000000000 ) ) ;
#48670=CARTESIAN_POINT ( 'NONE',  ( 0.000000000000000000, -2.500000000000000000, 0.000000000000000000 ) ) ;
#48756=CARTESIAN_POINT ( 'NONE',  ( 3.409440450231731923, 1.719598803866702719, -7.000000000000003553 ) ) ;
#48960=FILL_AREA_STYLE ('',( #55576 ) ) ;
#49092=FACE_OUTER_BOUND ( 'NONE', #41231, .T. ) ;
#49133=PLANE ( 'NONE',  #3728 ) ;
#49154=ORIENTED_EDGE ( 'NONE', *, *, #49992, .T. ) ;
#49210=CARTESIAN_POINT ( 'NONE',  ( -7.441974819423173848, -2.003239292658529180, 1.110121504110835877 ) ) ;
#49284=CARTESIAN_POINT ( 'NONE',  ( 0.000000000000000000, 2.000000000000000444, 0.000000000000000000 ) ) ;
#49290=VERTEX_POINT ( 'NONE', #58976 ) ;
#49438=AXIS2_PLACEMENT_3D ( 'NONE', #656, #37724, #48256 ) ;
#49443=EDGE_CURVE ( 'NONE', #45750, #7911, #2651, .T. ) ;
#49469=CARTESIAN_POINT ( 'NONE',  ( -5.705565085145811288, -2.472216779103303175, -4.117671386636410524 ) ) ;
#49482=CARTESIAN_POINT ( 'NONE',  ( 0.000000000000000000, 2.500000000000000000, 0.000000000000000000 ) ) ;
#49756=CARTESIAN_POINT ( 'NONE',  ( 2.418047948276646597, 2.101261491285135286, -7.000000000000001776 ) ) ;
#49786=DIRECTION ( 'NONE',  ( 1.000000000000000000, 0.000000000000000000, 0.000000000000000000 ) ) ;
#49992=EDGE_CURVE ( 'NONE', #30142, #45750, #47631, .T. ) ;
#50051=MANIFOLD_SOLID_BREP ( 'Chamfer1', #32879 ) ;
#50100=PLANE ( 'NONE',  #191 ) ;
#50148=UNCERTAINTY_MEASURE_WITH_UNIT (LENGTH_MEASURE( 1.000000000000000082E-05 ), #17944, 'distance_accuracy_value', 'NONE');
#50194=ORIENTED_EDGE ( 'NONE', *, *, #13495, .T. ) ;
#50201=EDGE_LOOP ( 'NONE', ( #30968, #41186, #12971 ) ) ;
#50246=ORIENTED_EDGE ( 'NONE', *, *, #49443, .T. ) ;
#50357=EDGE_CURVE ( 'NONE', #41509, #38350, #33351, .T. ) ;
#50436=EDGE_LOOP ( 'NONE', ( #39743, #25436, #47604 ) ) ;
#50459=LINE ( 'NONE', #16740, #66187 ) ;
#50680=EDGE_LOOP ( 'NONE', ( #49154, #50246, #51109, #32610, #23289, #14331 ) ) ;
#50754=EDGE_CURVE ( 'NONE', #40436, #3748, #54636, .T. ) ;
#50769=CIRCLE ( 'NONE', #31509, 6.999999999999997335 ) ;
#50796=EDGE_CURVE ( 'NONE', #13760, #30149, #15501, .T. ) ;
#51012=CARTESIAN_POINT ( 'NONE',  ( 3.409440450227774644, 1.719598803868655601, 7.000000000000001776 ) ) ;
#51075=FACE_OUTER_BOUND ( 'NONE', #67270, .T. ) ;
#51083=UNCERTAINTY_MEASURE_WITH_UNIT (LENGTH_MEASURE( 1.000000000000000082E-05 ), #19792, 'distance_accuracy_value', 'NONE');
#51109=ORIENTED_EDGE ( 'NONE', *, *, #23903, .T. ) ;
#51146=VERTEX_POINT ( 'NONE', #66290 ) ;
#51159=CARTESIAN_POINT ( 'NONE',  ( -6.239160159721276244, 2.499999999999999556, 3.193457606803197013 ) ) ;
#51253=CARTESIAN_POINT ( 'NONE',  ( -0.3558155365998594277, 2.493171897977953577, -7.000000000000002665 ) ) ;
#51265=EDGE_LOOP ( 'NONE', ( #33892, #43264, #35932, #51834 ) ) ;
#51313=VERTEX_POINT ( 'NONE', #5291 ) ;
#51401=CARTESIAN_POINT ( 'NONE',  ( -5.710692600061824997, 2.499999999999999112, 4.108790270285303414 ) ) ;
#51430=AXIS2_PLACEMENT_3D ( 'NONE', #29431, #30454, #19578 ) ;
#51497=DIRECTION ( 'NONE',  ( 0.000000000000000000, 0.000000000000000000, 1.000000000000000000 ) ) ;
#51506=VERTEX_POINT ( 'NONE', #25296 ) ;
#51542=EDGE_CURVE ( 'NONE', #24428, #58318, #19226, .T. ) ;
#51565=CARTESIAN_POINT ( 'NONE',  ( -7.511572993685801073E-16, 2.500000000000000000, 7.000000000000000888 ) ) ;
#51728=CARTESIAN_POINT ( 'NONE',  ( 4.041451884327377897, 1.417096231345241319, 7.000000000000000888 ) ) ;
#51834=ORIENTED_EDGE ( 'NONE', *, *, #36050, .F. ) ;
#51944=CONICAL_SURFACE ( 'NONE', #58649, 6.999999999999997335, 0.7853981633974500554 ) ;
#52011=EDGE_CURVE ( 'NONE', #10734, #25093, #43526, .T. ) ;
#52061=CARTESIAN_POINT ( 'NONE',  ( 0.000000000000000000, 2.500000000000000000, 0.000000000000000000 ) ) ;
#52109=VERTEX_POINT ( 'NONE', #34303 ) ;
#52115=ORIENTED_EDGE ( 'NONE', *, *, #50754, .F. ) ;
#52152=CARTESIAN_POINT ( 'NONE',  ( 0.000000000000000000, -2.500000000000000000, 0.000000000000000000 ) ) ;
#52244=DIRECTION ( 'NONE',  ( -0.000000000000000000, 1.000000000000000000, -0.000000000000000000 ) ) ;
#52408=PRODUCT ( '14. Nut M6', '14. Nut M6', '', ( #23386 ) ) ;
#52583=CYLINDRICAL_SURFACE ( 'NONE', #15, 3.000000000000000444 ) ;
#52658=CARTESIAN_POINT ( 'NONE',  ( 3.409440450231733699, -1.719598803866701386, -7.000000000000002665 ) ) ;
#52763=CARTESIAN_POINT ( 'NONE',  ( 7.766391886667106448, 1.733608113333017453, 0.5482146608018618750 ) ) ;
#52852=ORIENTED_EDGE ( 'NONE', *, *, #40619, .T. ) ;
#52862=EDGE_CURVE ( 'NONE', #15154, #30495, #1500, .T. ) ;
#52958=DIRECTION ( 'NONE',  ( 0.000000000000000000, -0.000000000000000000, 1.000000000000000000 ) ) ;
#53044=FACE_OUTER_BOUND ( 'NONE', #6462, .T. ) ;
#53081=CARTESIAN_POINT ( 'NONE',  ( -4.041451884327380562, -1.417096231345237545, -7.000000000000003553 ) ) ;
#53398=ORIENTED_EDGE ( 'NONE', *, *, #31392, .T. ) ;
#53420=AXIS2_PLACEMENT_3D ( 'NONE', #48276, #5653, #37749 ) ;
#53425=LINE ( 'NONE', #58336, #66300 ) ;
#53541=EDGE_CURVE ( 'NONE', #6283, #49290, #50769, .T. ) ;
#53563=CARTESIAN_POINT ( 'NONE',  ( -6.062177826491070398, 2.500000000000000000, -3.499999999999998224 ) ) ;
#53870=B_SPLINE_CURVE_WITH_KNOTS ( 'NONE', 3,
 ( #65009, #54115, #49210, #915, #54463, #38690, #32657, #12583 ),
 .UNSPECIFIED., .F., .F.,
 ( 4, 2, 2, 4 ),
 ( 2.544316211736544463E-07, 0.002094919859796806009, 0.003142252573884622008, 0.004189585287972438440 ),
 .UNSPECIFIED. ) ;
#53871=ORIENTED_EDGE ( 'NONE', *, *, #39756, .F. ) ;
#53883=DIRECTION ( 'NONE',  ( -0.000000000000000000, -1.000000000000000000, -0.000000000000000000 ) ) ;
#53969=FACE_BOUND ( 'NONE', #65359, .T. ) ;
#54112=AXIS2_PLACEMENT_3D ( 'NONE', #16125, #58651, #69548 ) ;
#54115=CARTESIAN_POINT ( 'NONE',  ( -7.766025168014157209, -1.733974831985841458, 0.5488498361408482573 ) ) ;
#54255=VECTOR ( 'NONE', #61562, 1000.000000000000000 ) ;
#54318=CARTESIAN_POINT ( 'NONE',  ( 2.755156416453790058, 1.983268963954968989, -7.000000000000002665 ) ) ;
#54321=B_SPLINE_CURVE_WITH_KNOTS ( 'NONE', 3,
 ( #32110, #61165, #56222, #65141, #23875, #17914 ),
 .UNSPECIFIED., .F., .F.,
 ( 4, 2, 4 ),
 ( 0.004189585287972440175, 0.006269578072783815043, 0.008349570857595189910 ),
 .UNSPECIFIED. ) ;
#54364=FACE_OUTER_BOUND ( 'NONE', #2710, .T. ) ;
#54391=CARTESIAN_POINT ( 'NONE',  ( 4.041451884327375232, 2.500000000000000000, -7.000000000000002665 ) ) ;
#54463=CARTESIAN_POINT ( 'NONE',  ( -6.767634268437465295, -2.367558512213881361, 2.278113600022078078 ) ) ;
#54580=DIRECTION ( 'NONE',  ( 0.000000000000000000, 0.000000000000000000, -1.000000000000000000 ) ) ;
#54636=B_SPLINE_CURVE_WITH_KNOTS ( 'NONE', 3,
 ( #8222, #46232, #45866, #2530, #14191, #18760, #25085, #24373 ),
 .UNSPECIFIED., .F., .F.,
 ( 4, 2, 2, 4 ),
 ( 2.544316211735810720E-07, 0.002094919859796807744, 0.003142252573884624176, 0.004189585287972440175 ),
 .UNSPECIFIED. ) ;
#54681=CARTESIAN_POINT ( 'NONE',  ( -7.511572993685801073E-16, 2.500000000000000000, 7.000000000000000888 ) ) ;
#54725=DIRECTION ( 'NONE',  ( 0.000000000000000000, -1.000000000000000000, 0.000000000000000000 ) ) ;
#54730=CARTESIAN_POINT ( 'NONE',  ( -6.759171781091400710, 2.392512705203732715, -2.292771058063876488 ) ) ;
#54789=ORIENTED_EDGE ( 'NONE', *, *, #16575, .T. ) ;
#55035=DIRECTION ( 'NONE',  ( 0.4999999999999998890, 0.000000000000000000, -0.8660254037844387076 ) ) ;
#55180=DIRECTION ( 'NONE',  ( 0.000000000000000000, 0.000000000000000000, 1.000000000000000000 ) ) ;
#55202=EDGE_CURVE ( 'NONE', #63907, #34321, #14982, .T. ) ;
#55448=CARTESIAN_POINT ( 'NONE',  ( -4.041451884327378785, -1.417096231345241542, 7.000000000000000000 ) ) ;
#55508=CARTESIAN_POINT ( 'NONE',  ( 0.000000000000000000, 2.500000000000000000, 0.000000000000000000 ) ) ;
#55576=FILL_AREA_STYLE_COLOUR ( '', #60646 ) ;
#55587=CARTESIAN_POINT ( 'NONE',  ( 6.062177826491067734, 2.500000000000000000, 3.500000000000000000 ) ) ;
#55750=EDGE_CURVE ( 'NONE', #25818, #51313, #66923, .T. ) ;
#55758=SHAPE_DEFINITION_REPRESENTATION ( #37285, #60355 ) ;
#55763=ORIENTED_EDGE ( 'NONE', *, *, #55750, .T. ) ;
#55849=VECTOR ( 'NONE', #61234, 1000.000000000000114 ) ;
#55869=CARTESIAN_POINT ( 'NONE',  ( 6.062177826491068622, -2.500000000000000000, -3.500000000000001332 ) ) ;
#55883=CARTESIAN_POINT ( 'NONE',  ( -0.7087670488515479539, -2.466410156631316131, 7.000000000000000000 ) ) ;
#55980=EDGE_CURVE ( 'NONE', #39091, #25818, #64514, .T. ) ;
#56033=FACE_OUTER_BOUND ( 'NONE', #3861, .T. ) ;
#56222=CARTESIAN_POINT ( 'NONE',  ( 5.365183871890737421, -2.392512705203734935, -4.707228941936126176 ) ) ;
#56298=DIRECTION ( 'NONE',  ( 0.000000000000000000, 1.000000000000000000, 0.000000000000000000 ) ) ;
#56513=AXIS2_PLACEMENT_3D ( 'NONE', #34846, #56298, #8131 ) ;
#56761=EDGE_LOOP ( 'NONE', ( #28712, #43413, #16372 ) ) ;
#56872=CIRCLE ( 'NONE', #68131, 6.999999999999997335 ) ;
#56968=DIRECTION ( 'NONE',  ( 0.000000000000000000, 0.000000000000000000, 1.000000000000000000 ) ) ;
#56973=CARTESIAN_POINT ( 'NONE',  ( 0.7093150608870635310, 2.499999999999996447, 7.000000000000000000 ) ) ;
#57019=AXIS2_PLACEMENT_3D ( 'NONE', #26010, #59069, #43307 ) ;
#57061=FACE_OUTER_BOUND ( 'NONE', #34395, .T. ) ;
#57145=CARTESIAN_POINT ( 'NONE',  ( 0.000000000000000000, 2.000000000000000444, 0.000000000000000000 ) ) ;
#57271=CARTESIAN_POINT ( 'NONE',  ( 6.759171781091399822, -2.392512705203733603, 2.292771058063876488 ) ) ;
#57296=DIRECTION ( 'NONE',  ( -0.000000000000000000, -1.000000000000000000, -0.000000000000000000 ) ) ;
#57315=CARTESIAN_POINT ( 'NONE',  ( 2.755156416437879674, 1.983268963961027920, 7.000000000000000888 ) ) ;
#57384=CARTESIAN_POINT ( 'NONE',  ( 0.000000000000000000, 2.500000000000000000, 0.000000000000000000 ) ) ;
#57640=ORIENTED_EDGE ( 'NONE', *, *, #10492, .F. ) ;
#57763=CARTESIAN_POINT ( 'NONE',  ( 5.705565085145809512, -2.472216779103305395, 4.117671386636410524 ) ) ;
#57820=LINE ( 'NONE', #4679, #67289 ) ;
#57867=AXIS2_PLACEMENT_3D ( 'NONE', #40097, #29129, #55180 ) ;
#58113=CARTESIAN_POINT ( 'NONE',  ( 5.356721384544673725, -2.367558512213880473, 4.721886399977921478 ) ) ;
#58146=EDGE_CURVE ( 'NONE', #38350, #41509, #34327, .T. ) ;
#58152=CYLINDRICAL_SURFACE ( 'NONE', #39550, 3.000000000000000444 ) ;
#58154=ADVANCED_FACE ( 'NONE', ( #31285 ), #30236, .F. ) ;
#58318=VERTEX_POINT ( 'NONE', #55869 ) ;
#58336=CARTESIAN_POINT ( 'NONE',  ( 8.082903768654761123, 2.500000000000000000, 9.511133375893962597E-16 ) ) ;
#58470=SURFACE_STYLE_FILL_AREA ( #8893 ) ;
#58620=AXIS2_PLACEMENT_3D ( 'NONE', #66651, #18465, #51497 ) ;
#58649=AXIS2_PLACEMENT_3D ( 'NONE', #35310, #45201, #34261 ) ;
#58651=DIRECTION ( 'NONE',  ( 0.000000000000000000, -1.000000000000000000, 0.000000000000000000 ) ) ;
#58976=CARTESIAN_POINT ( 'NONE',  ( 6.062177826491067734, -2.500000000000000000, 3.500000000000000000 ) ) ;
#59069=DIRECTION ( 'NONE',  ( 0.8660254037844387076, 0.000000000000000000, -0.5000000000000000000 ) ) ;
#59150=ORIENTED_EDGE ( 'NONE', *, *, #44925, .F. ) ;
#59157=DIRECTION ( 'NONE',  ( 0.000000000000000000, 1.000000000000000000, 0.000000000000000000 ) ) ;
#59279=EDGE_CURVE ( 'NONE', #63065, #6283, #59909, .T. ) ;
#59350=CARTESIAN_POINT ( 'NONE',  ( -0.3558155365998603159, -2.493171897977953133, -7.000000000000004441 ) ) ;
#59358=ORIENTED_EDGE ( 'NONE', *, *, #36050, .T. ) ;
#59434=CARTESIAN_POINT ( 'NONE',  ( 0.000000000000000000, 2.000000000000000444, 3.000000000000000444 ) ) ;
#59717=EDGE_LOOP ( 'NONE', ( #55763, #17679, #20136 ) ) ;
#59832=ADVANCED_FACE ( 'NONE', ( #17198 ), #21465, .T. ) ;
#59909=B_SPLINE_CURVE_WITH_KNOTS ( 'NONE', 3,
 ( #66438, #29495, #39396, #18255, #39742, #55883, #28429, #45379, #65753 ),
 .UNSPECIFIED., .F., .F.,
 ( 4, 2, 1, 2, 4 ),
 ( 0.007659788818331632332, 0.009746199297478889273, 0.01078940453705251774, 0.01131100715683933111, 0.01183260977662614621 ),
 .UNSPECIFIED. ) ;
#59977=CARTESIAN_POINT ( 'NONE',  ( 0.000000000000000000, 0.000000000000000000, 0.000000000000000000 ) ) ;
#60156=CARTESIAN_POINT ( 'NONE',  ( 0.000000000000000000, -2.500000000000000000, 0.000000000000000000 ) ) ;
#60204=EDGE_CURVE ( 'NONE', #7911, #30495, #39516, .T. ) ;
#60355=SHAPE_REPRESENTATION ( '14. Nut M6', ( #42840 ), #1086 ) ;
#60356=DIRECTION ( 'NONE',  ( -0.000000000000000000, -1.000000000000000000, -0.000000000000000000 ) ) ;
#60360=CARTESIAN_POINT ( 'NONE',  ( 0.000000000000000000, 2.500000000000000000, 0.000000000000000000 ) ) ;
#60400=DIRECTION ( 'NONE',  ( 0.000000000000000000, 0.000000000000000000, 1.000000000000000000 ) ) ;
#60574=ADVANCED_FACE ( 'NONE', ( #10172 ), #16024, .T. ) ;
#60646=COLOUR_RGB ( '', 0.08235294, 0.09019608, 0.10196078) ;
#60703=CARTESIAN_POINT ( 'NONE',  ( -6.413663052920317575, 2.499999999999997780, -2.891209729714699250 ) ) ;
#60716=CARTESIAN_POINT ( 'NONE',  ( 0.000000000000000000, -2.500000000000000000, 3.000000000000000444 ) ) ;
#60893=ORIENTED_EDGE ( 'NONE', *, *, #46096, .T. ) ;
#61052=B_SPLINE_CURVE_WITH_KNOTS ( 'NONE', 3,
 ( #9647, #35671, #20156, #46619, #8929, #25446, #51159, #3602 ),
 .UNSPECIFIED., .F., .F.,
 ( 4, 2, 2, 4 ),
 ( 2.544316211735811779E-07, 0.002094919859796806009, 0.003142252573884622008, 0.004189585287972438440 ),
 .UNSPECIFIED. ) ;
#61070=CARTESIAN_POINT ( 'NONE',  ( -0.7087670488515470657, 2.466410156631316131, 7.000000000000000000 ) ) ;
#61073=LINE ( 'NONE', #60716, #39641 ) ;
#61165=CARTESIAN_POINT ( 'NONE',  ( 5.710692600061823221, -2.500000000000000000, -4.108790270285303414 ) ) ;
#61232=ORIENTED_EDGE ( 'NONE', *, *, #32031, .F. ) ;
#61234=DIRECTION ( 'NONE',  ( 8.659560562354962440E-17, 0.7071067811865451302, -0.7071067811865500152 ) ) ;
#61488=CARTESIAN_POINT ( 'NONE',  ( 8.082903768654761123, -1.417096231345241097, 9.294316082458970795E-16 ) ) ;
#61562=DIRECTION ( 'NONE',  ( 0.000000000000000000, -0.7071067811865496822, -0.7071067811865453523 ) ) ;
#61641=DIRECTION ( 'NONE',  ( 0.000000000000000000, 1.000000000000000000, 0.000000000000000000 ) ) ;
#61649=AXIS2_PLACEMENT_3D ( 'NONE', #26965, #21033, #10830 ) ;
#61674=CIRCLE ( 'NONE', #46014, 6.999999999999997335 ) ;
#61696=FACE_OUTER_BOUND ( 'NONE', #64864, .T. ) ;
#61758=EDGE_CURVE ( 'NONE', #58318, #49290, #8265, .T. ) ;
#61834=ORIENTED_EDGE ( 'NONE', *, *, #52862, .F. ) ;
#61921=ORIENTED_EDGE ( 'NONE', *, *, #4998, .F. ) ;
#62179=EDGE_CURVE ( 'NONE', #28517, #12794, #35329, .T. ) ;
#62187=CARTESIAN_POINT ( 'NONE',  ( -6.062177826491070398, -2.500000000000000000, -3.499999999999998224 ) ) ;
#62303=AXIS2_PLACEMENT_3D ( 'NONE', #22199, #16269, #33107 ) ;
#62307=VECTOR ( 'NONE', #64746, 1000.000000000000114 ) ;
#62365=CARTESIAN_POINT ( 'NONE',  ( -7.440601873764705054, -2.005109422339667269, -1.112499515747341183 ) ) ;
#62669=DIRECTION ( 'NONE',  ( 0.5000000000000003331, 0.000000000000000000, 0.8660254037844383745 ) ) ;
#62762=DIRECTION ( 'NONE',  ( 0.000000000000000000, 1.000000000000000000, 0.000000000000000000 ) ) ;
#63017=CARTESIAN_POINT ( 'NONE',  ( 6.062177826491067734, -2.500000000000000000, 3.500000000000000000 ) ) ;
#63065=VERTEX_POINT ( 'NONE', #64469 ) ;
#63545=ORIENTED_EDGE ( 'NONE', *, *, #58146, .T. ) ;
#63736=CARTESIAN_POINT ( 'NONE',  ( 4.683753779217428637, 2.005109422339667269, -5.887500484252663036 ) ) ;
#63907=VERTEX_POINT ( 'NONE', #54681 ) ;
#64086=CARTESIAN_POINT ( 'NONE',  ( 4.357963766315029019, 1.733608113333017897, -6.451785339198144342 ) ) ;
#64374=CARTESIAN_POINT ( 'NONE',  ( -4.683753779217433078, 2.005109422339666825, 5.887500484252660371 ) ) ;
#64469=CARTESIAN_POINT ( 'NONE',  ( -4.041451884327378785, -1.417096231345241542, 7.000000000000000000 ) ) ;
#64514=CIRCLE ( 'NONE', #18426, 6.999999999999997335 ) ;
#64546=ORIENTED_EDGE ( 'NONE', *, *, #50357, .T. ) ;
#64604=CARTESIAN_POINT ( 'NONE',  ( -4.682380833558966060, -2.003239292658526516, -5.889878495889164789 ) ) ;
#64627=CARTESIAN_POINT ( 'NONE',  ( -4.041451884327378785, 2.500000000000000000, 7.000000000000000000 ) ) ;
#64671=CARTESIAN_POINT ( 'NONE',  ( 6.418790567836325955, -2.472216779103306283, -2.882328613363592584 ) ) ;
#64746=DIRECTION ( 'NONE',  ( 0.000000000000000000, 0.7071067811865451302, 0.7071067811865500152 ) ) ;
#64748=CARTESIAN_POINT ( 'NONE',  ( -4.358330484967981810, 1.733974831985838794, -6.451150163859153963 ) ) ;
#64864=EDGE_LOOP ( 'NONE', ( #64924, #69614, #22495, #17746 ) ) ;
#64872=EDGE_CURVE ( 'NONE', #51146, #63065, #42687, .T. ) ;
#64924=ORIENTED_EDGE ( 'NONE', *, *, #50796, .T. ) ;
#64941=CARTESIAN_POINT ( 'NONE',  ( 0.000000000000000000, 2.500000000000000000, 0.000000000000000000 ) ) ;
#65009=CARTESIAN_POINT ( 'NONE',  ( -8.082903768654761123, -1.417096231345241097, -1.759977097422839922E-15 ) ) ;
#65025=EDGE_CURVE ( 'NONE', #6283, #25093, #39298, .T. ) ;
#65081=FACE_OUTER_BOUND ( 'NONE', #15439, .T. ) ;
#65141=CARTESIAN_POINT ( 'NONE',  ( 4.683753779217428637, -2.005109422339667269, -5.887500484252663036 ) ) ;
#65302=DIRECTION ( 'NONE',  ( -0.000000000000000000, -1.000000000000000000, -0.000000000000000000 ) ) ;
#65359=EDGE_LOOP ( 'NONE', ( #63545, #64546 ) ) ;
#65378=ORIENTED_EDGE ( 'NONE', *, *, #47865, .F. ) ;
#65403=EDGE_CURVE ( 'NONE', #67895, #51506, #29013, .T. ) ;
#65441=PRESENTATION_STYLE_ASSIGNMENT (( #43360 ) ) ;
#65444=AXIS2_PLACEMENT_3D ( 'NONE', #32419, #53883, #54580 ) ;
#65606=PLANE ( 'NONE',  #12926 ) ;
#65633=CARTESIAN_POINT ( 'NONE',  ( -6.062177826491070398, -2.500000000000000000, -3.499999999999998224 ) ) ;
#65674=EDGE_CURVE ( 'NONE', #49290, #24428, #18933, .T. ) ;
#65692=CARTESIAN_POINT ( 'NONE',  ( 0.000000000000000000, -2.500000000000000000, 0.000000000000000000 ) ) ;
#65753=CARTESIAN_POINT ( 'NONE',  ( -7.511572993685798115E-16, -2.500000000000000000, 6.999999999999997335 ) ) ;
#65812=ORIENTED_EDGE ( 'NONE', *, *, #10579, .F. ) ;
#65813=AXIS2_PLACEMENT_3D ( 'NONE', #24289, #41907, #41538 ) ;
#65892=VECTOR ( 'NONE', #42348, 1000.000000000000000 ) ;
#65945=ORIENTED_EDGE ( 'NONE', *, *, #39762, .F. ) ;
#66027=CARTESIAN_POINT ( 'NONE',  ( -3.414270897523325132, 1.730686724747263705, -7.000000000000004441 ) ) ;
#66050=DIRECTION ( 'NONE',  ( 0.000000000000000000, 0.000000000000000000, 1.000000000000000000 ) ) ;
#66187=VECTOR ( 'NONE', #32904, 1000.000000000000000 ) ;
#66200=VECTOR ( 'NONE', #65302, 1000.000000000000000 ) ;
#66240=ORIENTED_EDGE ( 'NONE', *, *, #4778, .T. ) ;
#66290=CARTESIAN_POINT ( 'NONE',  ( -6.062177826491069510, -2.500000000000000000, 3.499999999999999556 ) ) ;
#66300=VECTOR ( 'NONE', #31236, 1000.000000000000000 ) ;
#66328=PRODUCT_DEFINITION_FORMATION_WITH_SPECIFIED_SOURCE ( 'ANY', '', #52408, .NOT_KNOWN. ) ;
#66438=CARTESIAN_POINT ( 'NONE',  ( -4.041451884327378785, -1.417096231345241542, 7.000000000000000000 ) ) ;
#66485=ADVANCED_FACE ( 'NONE', ( #67671 ), #48193, .T. ) ;
#66650=EDGE_CURVE ( 'NONE', #51313, #4242, #57820, .T. ) ;
#66651=CARTESIAN_POINT ( 'NONE',  ( 0.000000000000000000, 2.000000000000000444, 0.000000000000000000 ) ) ;
#66807=CARTESIAN_POINT ( 'NONE',  ( 7.766391886667106448, -1.733608113333017453, 0.5482146608018618750 ) ) ;
#66886=FACE_OUTER_BOUND ( 'NONE', #30502, .T. ) ;
#66907=ORIENTED_EDGE ( 'NONE', *, *, #44925, .T. ) ;
#66923=B_SPLINE_CURVE_WITH_KNOTS ( 'NONE', 3,
 ( #1576, #60703, #54730, #17152, #851, #23102 ),
 .UNSPECIFIED., .F., .F.,
 ( 4, 2, 4 ),
 ( 0.004189585287972440175, 0.006269578072783811573, 0.008349570857595182971 ),
 .UNSPECIFIED. ) ;
#66925=AXIS2_PLACEMENT_3D ( 'NONE', #20041, #67557, #36280 ) ;
#67270=EDGE_LOOP ( 'NONE', ( #60893, #32356, #20912 ) ) ;
#67289=VECTOR ( 'NONE', #3601, 1000.000000000000000 ) ;
#67299=FACE_BOUND ( 'NONE', #338, .T. ) ;
#67384=ORIENTED_EDGE ( 'NONE', *, *, #52011, .T. ) ;
#67431=CARTESIAN_POINT ( 'NONE',  ( 3.728455551740340823, -1.573594397638760745, -7.000000000000004441 ) ) ;
#67557=DIRECTION ( 'NONE',  ( -0.000000000000000000, -1.000000000000000000, -0.000000000000000000 ) ) ;
#67624=PLANE ( 'NONE',  #69134 ) ;
#67671=FACE_OUTER_BOUND ( 'NONE', #50436, .T. ) ;
#67832=CIRCLE ( 'NONE', #22899, 3.000000000000000444 ) ;
#67895=VERTEX_POINT ( 'NONE', #23635 ) ;
#68131=AXIS2_PLACEMENT_3D ( 'NONE', #55508, #17881, #66050 ) ;
#68144=CARTESIAN_POINT ( 'NONE',  ( 7.511572993685799101E-16, -2.500000000000000000, -6.999999999999997335 ) ) ;
#68327=ADVANCED_FACE ( 'NONE', ( #10142 ), #22363, .T. ) ;
#68652=( LENGTH_UNIT ( ) NAMED_UNIT ( * ) SI_UNIT ( .MILLI., .METRE. ) );
#68709=CARTESIAN_POINT ( 'NONE',  ( 0.000000000000000000, -2.500000000000000000, 0.000000000000000000 ) ) ;
#68796=EDGE_CURVE ( 'NONE', #13760, #42774, #50459, .T. ) ;
#69038=CARTESIAN_POINT ( 'NONE',  ( 5.710692600061823221, 2.500000000000000000, -4.108790270285303414 ) ) ;
#69134=AXIS2_PLACEMENT_3D ( 'NONE', #9240, #30663, #62669 ) ;
#69293=CARTESIAN_POINT ( 'NONE',  ( 5.705565085145809512, 2.472216779103305395, 4.117671386636410524 ) ) ;
#69382=CARTESIAN_POINT ( 'NONE',  ( 6.062177826491068622, 2.500000000000000000, -3.500000000000001332 ) ) ;
#69548=DIRECTION ( 'NONE',  ( 0.000000000000000000, 0.000000000000000000, 1.000000000000000000 ) ) ;
#69607=CARTESIAN_POINT ( 'NONE',  ( 6.413663052920311358, 2.499999999999998668, 2.891209729714698806 ) ) ;
#69614=ORIENTED_EDGE ( 'NONE', *, *, #12199, .T. ) ;
ENDSEC;
END-ISO-10303-21;
